ISO-10303-21;
HEADER;
FILE_DESCRIPTION (('STEP AP214'),
    '1' );
FILE_NAME ('Nut.step',
    '2026-10-06T09:00:30',
    ( '' ),
    ( '' ),
    'SwSTEP 2.0',
    'SolidWorks 2020',
    '' );
FILE_SCHEMA (( 'AUTOMOTIVE_DESIGN' ));
ENDSEC;

DATA;
#53=VERTEX_POINT ( 'NONE', #11043 ) ;
#108=CARTESIAN_POINT ( 'NONE',  ( 0.000000000000000000, 0.000000000000000000, 229.2412452700000074 ) ) ;
#120=CARTESIAN_POINT ( 'NONE',  ( 1.007237960741799165, 1.747572776708515185, 227.6412452700616598 ) ) ;
#155=DIRECTION ( 'NONE',  ( 0.000000000000000000, 0.000000000000000000, -1.000000000000000000 ) ) ;
#167=EDGE_CURVE ( 'NONE', #31001, #29368, #18432, .T. ) ;
#195=CARTESIAN_POINT ( 'NONE',  ( -0.6197578587862698773, -3.499936541734924411, 230.8124538892490136 ) ) ;
#206=ORIENTED_EDGE ( 'NONE', *, *, #14101, .F. ) ;
#216=CIRCLE ( 'NONE', #11262, 3.491271820589999741 ) ;
#303=B_SPLINE_CURVE_WITH_KNOTS ( 'NONE', 3,
 ( #7112, #10096, #12136, #9624, #26931, #23962, #26313, #16696, #28976, #19692, #29276, #195, #19386, #5366, #24571, #11984, #24252, #21910, #9939, #19542, #7719, #4759, #14973, #3006, #12599, #31031 ),
 .UNSPECIFIED., .F., .F.,
 ( 4, 2, 2, 1, 1, 2, 2, 2, 2, 2, 1, 1, 2, 2, 4 ),
 ( 0.000000000000000000, 0.1250000000000129896, 0.1875000000000214828, 0.2187500000000258127, 0.2343750000000295874, 0.2421875000000298650, 0.2500000000000301426, 0.5000000000000094369, 0.6249999999999991118, 0.6874999999999938938, 0.7187499999999913403, 0.7343749999999900080, 0.7421874999999908962, 0.7499999999999916733, 1.000000000000000000 ),
 .UNSPECIFIED. ) ;
#311=CARTESIAN_POINT ( 'NONE',  ( -0.9568679087069641431, 3.499999999999999556, 230.7624477058865295 ) ) ;
#334=EDGE_LOOP ( 'NONE', ( #15122, #20536, #2916, #30946, #21769, #8369 ) ) ;
#339=SHAPE_REPRESENTATION ( 'Nut', ( #17722 ), #14741 ) ;
#372=DIRECTION ( 'NONE',  ( 0.000000000000000000, 0.000000000000000000, -1.000000000000000000 ) ) ;
#412=EDGE_CURVE ( 'NONE', #27661, #8534, #216, .T. ) ;
#424=CARTESIAN_POINT ( 'NONE',  ( 3.370970677400644266, 1.161062029669245321, 227.6835602974635719 ) ) ;
#448=ORIENTED_EDGE ( 'NONE', *, *, #167, .T. ) ;
#454=SURFACE_STYLE_FILL_AREA ( #9717 ) ;
#518=B_SPLINE_CURVE_WITH_KNOTS ( 'NONE', 3,
 ( #27708, #6155, #1766, #15753, #13874, #1917, #25838, #4277, #13558, #25368, #23481, #21112, #6786, #30708, #3806, #28337, #13394, #9135, #23165, #23005 ),
 .UNSPECIFIED., .F., .F.,
 ( 4, 1, 1, 1, 2, 2, 2, 1, 1, 1, 2, 2, 4 ),
 ( 0.000000000000000000, 0.1249999999999770739, 0.1874999999999654166, 0.2187499999999614197, 0.2343749999999610867, 0.2499999999999607536, 0.4999999999999691358, 0.6249999999999732436, 0.6874999999999761302, 0.7187499999999775735, 0.7343749999999796829, 0.7499999999999819034, 1.000000000000000000 ),
 .UNSPECIFIED. ) ;
#540=MANIFOLD_SOLID_BREP ( 'PartBody', #13552 ) ;
#674=ORIENTED_EDGE ( 'NONE', *, *, #8406, .F. ) ;
#696=DIRECTION ( 'NONE',  ( -0.8660254037843290176, 0.5000000000001900702, 0.000000000000000000 ) ) ;
#719=DIRECTION ( 'NONE',  ( 0.000000000000000000, -1.000000000000000000, 0.000000000000000000 ) ) ;
#726=CARTESIAN_POINT ( 'NONE',  ( 3.221703195401058650, 1.419518900322475741, 227.6563758784883191 ) ) ;
#977=ORIENTED_EDGE ( 'NONE', *, *, #11138, .T. ) ;
#978=AXIS2_PLACEMENT_3D ( 'NONE', #18506, #25756, #719 ) ;
#995=ADVANCED_FACE ( 'NONE', ( #23367 ), #9025, .T. ) ;
#1027=CARTESIAN_POINT ( 'NONE',  ( 3.685684228007439778, 0.6162076564309076909, 230.7072465799053020 ) ) ;
#1065=AXIS2_PLACEMENT_3D ( 'NONE', #30651, #18673, #6410 ) ;
#1169=COLOUR_RGB ( '', 0.40784314, 0.44705882, 0.49803922) ;
#1174=CARTESIAN_POINT ( 'NONE',  ( 0.000000000000000000, 0.000000000000000000, 227.6412452699999847 ) ) ;
#1200=PRESENTATION_STYLE_ASSIGNMENT (( #17855 ) ) ;
#1222=CARTESIAN_POINT ( 'NONE',  ( -2.837346519424604807, 2.085571669681350659, 230.8270369382007630 ) ) ;
#1258=CARTESIAN_POINT ( 'NONE',  ( -3.511528848185079266, -0.9178490657093262284, 227.7210190899423310 ) ) ;
#1267=CARTESIAN_POINT ( 'NONE',  ( -3.538182117160495022, 0.8713469530890178838, 227.7293001947007269 ) ) ;
#1341=DIRECTION ( 'NONE',  ( 0.000000000000000000, 0.000000000000000000, -1.000000000000000000 ) ) ;
#1352=APPLICATION_CONTEXT ( 'automotive_design' ) ;
#1380=CARTESIAN_POINT ( 'NONE',  ( -3.542173841662227485, 0.8647749370036884597, 230.7522105547303966 ) ) ;
#1414=CARTESIAN_POINT ( 'NONE',  ( 1.949119511211575118, 0.5206197137392853946, 230.8412452700000301 ) ) ;
#1438=ORIENTED_EDGE ( 'NONE', *, *, #28112, .T. ) ;
#1465=DIRECTION ( 'NONE',  ( 0.000000000000000000, 0.000000000000000000, -1.000000000000000000 ) ) ;
#1582=CARTESIAN_POINT ( 'NONE',  ( -3.521608956067899587, 0.9000755979543652030, 227.7241098089399713 ) ) ;
#1590=CARTESIAN_POINT ( 'NONE',  ( 1.275182700919280654, -3.500000000000000444, 227.7673180537732947 ) ) ;
#1621=ORIENTED_EDGE ( 'NONE', *, *, #22367, .F. ) ;
#1689=CONICAL_SURFACE ( 'NONE', #23821, 3.491271820449999286, 1.047197551199999799 ) ;
#1735=CARTESIAN_POINT ( 'NONE',  ( -2.208189912596424609, 3.175302878607322743, 227.8506595042306060 ) ) ;
#1743=CARTESIAN_POINT ( 'NONE',  ( 2.400053023253180040, 2.842866040618700296, 230.7188131565947629 ) ) ;
#1745=CARTESIAN_POINT ( 'NONE',  ( 0.1546076948666131046, -3.500000000000000000, 227.6466545571240943 ) ) ;
#1766=CARTESIAN_POINT ( 'NONE',  ( 2.256478611577762194, -3.091664398557809168, 227.8316576175172656 ) ) ;
#1774=CARTESIAN_POINT ( 'NONE',  ( 0.7992118188004544432, 3.499831230570420004, 227.6979960600617119 ) ) ;
#1776=LINE ( 'NONE', #16234, #8698 ) ;
#1917=CARTESIAN_POINT ( 'NONE',  ( 2.520003984824367826, -2.635225063011365609, 227.7302799852730288 ) ) ;
#2017=CARTESIAN_POINT ( 'NONE',  ( 3.479864333095661344, -0.9723755506658986469, 230.7708768453293260 ) ) ;
#2042=CARTESIAN_POINT ( 'NONE',  ( 0.8979745064479516259, 3.499999999999999112, 230.7711489403451424 ) ) ;
#2198=CARTESIAN_POINT ( 'NONE',  ( -0.3083106915816442584, 3.499999999999999556, 230.8358029176229138 ) ) ;
#2289=ORIENTED_EDGE ( 'NONE', *, *, #11138, .F. ) ;
#2324=CARTESIAN_POINT ( 'NONE',  ( 2.000000000000000000, -0.2617993877991515728, 227.6412452702004430 ) ) ;
#2325=PRODUCT_DEFINITION ( 'UNKNOWN', '', #16358, #30748 ) ;
#2338=VERTEX_POINT ( 'NONE', #27096 ) ;
#2351=EDGE_CURVE ( 'NONE', #8650, #53, #9956, .T. ) ;
#2353=CARTESIAN_POINT ( 'NONE',  ( 2.020725942159999899, 3.500000000000000000, 230.5235986622430175 ) ) ;
#2446=DIRECTION ( 'NONE',  ( 0.000000000000000000, -1.000000000000000000, 0.000000000000000000 ) ) ;
#2472=CARTESIAN_POINT ( 'NONE',  ( 0.2617993877991493523, 1.999999999999999556, 227.6412452700154176 ) ) ;
#2621=CARTESIAN_POINT ( 'NONE',  ( 1.747572776708514519, -1.007237960741800720, 227.6412452702466283 ) ) ;
#2627=CARTESIAN_POINT ( 'NONE',  ( 0.000000000000000000, 0.000000000000000000, 0.000000000000000000 ) ) ;
#2679=CARTESIAN_POINT ( 'NONE',  ( -2.020725942109999895, 3.500000000090000007, 227.9588918784999976 ) ) ;
#2716=VECTOR ( 'NONE', #7230, 1000.000000000000000 ) ;
#2791=ORIENTED_EDGE ( 'NONE', *, *, #5209, .F. ) ;
#2799=CARTESIAN_POINT ( 'NONE',  ( -2.449212707639999657E-16, 2.000000000000000000, 229.2412452703699728 ) ) ;
#2916=ORIENTED_EDGE ( 'NONE', *, *, #2351, .T. ) ;
#2930=B_SPLINE_CURVE_WITH_KNOTS ( 'NONE', 3,
 ( #11893, #31094, #14885, #19443, #9537, #28725, #29034, #7628, #1027, #22729, #17534 ),
 .UNSPECIFIED., .F., .F.,
 ( 4, 1, 1, 1, 2, 2, 4 ),
 ( 0.000000000000000000, 0.2500000000000151545, 0.3750000000000210387, 0.4375000000000270894, 0.4687500000000269784, 0.5000000000000268674, 1.000000000000000000 ),
 .UNSPECIFIED. ) ;
#2944=VERTEX_POINT ( 'NONE', #15796 ) ;
#2960=DIRECTION ( 'NONE',  ( -0.7600087925169251024, -0.4151946956549595336, 0.4999999999969509945 ) ) ;
#2965=EDGE_CURVE ( 'NONE', #26221, #18457, #27720, .T. ) ;
#2970=AXIS2_PLACEMENT_3D ( 'NONE', #23758, #11788, #21394 ) ;
#3006=CARTESIAN_POINT ( 'NONE',  ( 1.290941959522689864, -3.499733189061704053, 230.7123227554298239 ) ) ;
#3034=PLANE ( 'NONE',  #12724 ) ;
#3165=B_SPLINE_CURVE_WITH_KNOTS ( 'NONE', 3,
 ( #28898, #2472, #11602, #120, #28435, #23885, #4981, #19457, #9700, #2324, #4522, #2621, #28593, #11753, #29050, #21360, #30955, #9382 ),
 .UNSPECIFIED., .F., .F.,
 ( 4, 2, 2, 2, 2, 2, 2, 2, 4 ),
 ( 0.000000000000000000, 0.1250000000000000000, 0.2500000000000000000, 0.3750000000000000000, 0.5000000000000000000, 0.6250000000000000000, 0.7500000000000000000, 0.8750000000000000000, 1.000000000000000000 ),
 .UNSPECIFIED. ) ;
#3245=ORIENTED_EDGE ( 'NONE', *, *, #10974, .T. ) ;
#3317=ORIENTED_EDGE ( 'NONE', *, *, #28321, .F. ) ;
#3476=DIRECTION ( 'NONE',  ( -0.5000000000001899592, 0.8660254037843289066, 0.000000000000000000 ) ) ;
#3515=AXIS2_PLACEMENT_3D ( 'NONE', #22889, #11551, #13433 ) ;
#3546=AXIS2_PLACEMENT_3D ( 'NONE', #7557, #4738, #19370 ) ;
#3547=( NAMED_UNIT ( * ) PLANE_ANGLE_UNIT ( ) SI_UNIT ( $, .RADIAN. ) );
#3560=CARTESIAN_POINT ( 'NONE',  ( -3.483928249568471358, -0.9656592618177964882, 230.7696496080388329 ) ) ;
#3617=CARTESIAN_POINT ( 'NONE',  ( 2.990544846595957651, 1.820224383385054212, 230.8378734041668565 ) ) ;
#3619=CARTESIAN_POINT ( 'NONE',  ( 0.3874847876441021577, -3.500000000000000888, 227.6554536018038561 ) ) ;
#3701=B_SPLINE_CURVE_WITH_KNOTS ( 'NONE', 3,
 ( #30163, #10975, #20566, #23100, #8595, #1380, #11131, #11290, #18367, #18034, #20729, #1222, #20894, #13645, #8434, #28270, #11445, #30000, #8916, #10821 ),
 .UNSPECIFIED., .F., .F.,
 ( 4, 1, 1, 1, 2, 2, 2, 1, 1, 1, 2, 2, 4 ),
 ( 0.000000000000000000, 0.1250000000000162925, 0.1875000000000264511, 0.2187500000000315026, 0.2343750000000323075, 0.2500000000000330846, 0.5000000000000234257, 0.6250000000000184297, 0.6875000000000157652, 0.7187500000000145439, 0.7343750000000153211, 0.7500000000000160982, 1.000000000000000000 ),
 .UNSPECIFIED. ) ;
#3729=CARTESIAN_POINT ( 'NONE',  ( -2.594691348381471308, -2.505853015390347771, 230.7743357003607230 ) ) ;
#3767=CARTESIAN_POINT ( 'NONE',  ( -3.484101657925389173, -0.9653352591375119474, 227.7128614111470597 ) ) ;
#3775=CARTESIAN_POINT ( 'NONE',  ( -2.219613442066195930, -3.155516745172294080, 227.8440641264227793 ) ) ;
#3786=CARTESIAN_POINT ( 'NONE',  ( 2.594691348412234255, 2.505853015323757038, 230.7743357003746496 ) ) ;
#3806=CARTESIAN_POINT ( 'NONE',  ( 3.460344806775433657, -1.006506982961865582, 227.7058346192795852 ) ) ;
#3882=CARTESIAN_POINT ( 'NONE',  ( -3.685684228003564655, -0.6162076564376223198, 230.7072465799074905 ) ) ;
#3902=CARTESIAN_POINT ( 'NONE',  ( 3.489756073974365602, -0.9552379302931907068, 230.7680100055977732 ) ) ;
#3923=CARTESIAN_POINT ( 'NONE',  ( 0.2653940490574222544, -2.000000000000000444, 230.8412452700000301 ) ) ;
#3925=VECTOR ( 'NONE', #20505, 1000.000000000000227 ) ;
#3943=CARTESIAN_POINT ( 'NONE',  ( -1.238178402523181232, -3.500000000000000000, 227.7677604876802491 ) ) ;
#3986=ORIENTED_EDGE ( 'NONE', *, *, #18675, .T. ) ;
#4059=CARTESIAN_POINT ( 'NONE',  ( 3.494141269252792448, -0.9476394297810019074, 230.7667222917565937 ) ) ;
#4089=CARTESIAN_POINT ( 'NONE',  ( -2.874794789347344892, 2.020489689856069582, 227.6523062920440736 ) ) ;
#4124=CARTESIAN_POINT ( 'NONE',  ( 0.1574870170871346953, 3.500159137053637348, 227.6463841914532509 ) ) ;
#4201=CARTESIAN_POINT ( 'NONE',  ( -2.620483857012521511, -2.461162703801856644, 230.7813955785499047 ) ) ;
#4211=CARTESIAN_POINT ( 'NONE',  ( 2.340434223344346254, -2.945736553369034283, 230.6852868990013405 ) ) ;
#4247=CARTESIAN_POINT ( 'NONE',  ( -3.510560880917136473, 0.9192256959274132111, 227.7207037332345863 ) ) ;
#4277=CARTESIAN_POINT ( 'NONE',  ( 2.552654958872357049, -2.578671917043665385, 227.7200428341182317 ) ) ;
#4282=CARTESIAN_POINT ( 'NONE',  ( 2.020725942159999899, -3.500000000000000000, 229.2412452703699728 ) ) ;
#4317=ORIENTED_EDGE ( 'NONE', *, *, #20014, .F. ) ;
#4335=ORIENTED_EDGE ( 'NONE', *, *, #7284, .F. ) ;
#4368=CARTESIAN_POINT ( 'NONE',  ( 3.109970238519766728, -1.613691810954662298, 230.8361063485526188 ) ) ;
#4398=CARTESIAN_POINT ( 'NONE',  ( -3.676689958403109859, 0.6312712462375396072, 227.7788113689686895 ) ) ;
#4502=EDGE_CURVE ( 'NONE', #18566, #11709, #2930, .T. ) ;
#4522=CARTESIAN_POINT ( 'NONE',  ( 1.947945353336630880, -0.5234957687185622932, 227.6412452702158475 ) ) ;
#4527=CARTESIAN_POINT ( 'NONE',  ( 2.874206261753454061, -2.022079741049881196, 230.8361203540554527 ) ) ;
#4640=PLANE ( 'NONE',  #22305 ) ;
#4688=PRESENTATION_STYLE_ASSIGNMENT (( #10037 ) ) ;
#4702=CARTESIAN_POINT ( 'NONE',  ( 1.275182700913060962, 3.500000000000000444, 230.7151724862288233 ) ) ;
#4710=DIRECTION ( 'NONE',  ( 0.8775825618903722036, 0.4794255386042040601, 0.000000000000000000 ) ) ;
#4715=AXIS2_PLACEMENT_3D ( 'NONE', #7534, #29088, #19346 ) ;
#4717=ORIENTED_EDGE ( 'NONE', *, *, #28112, .F. ) ;
#4738=DIRECTION ( 'NONE',  ( 0.000000000000000000, 0.000000000000000000, 1.000000000000000000 ) ) ;
#4750=B_SPLINE_CURVE_WITH_KNOTS ( 'NONE', 3,
 ( #16965, #26263, #24209, #17119, #28622, #19021, #19337, #311, #11296, #2198, #14000, #9581, #12243, #29080, #9729, #2042, #28928, #4702, #7524, #19178 ),
 .UNSPECIFIED., .F., .F.,
 ( 4, 1, 1, 1, 2, 2, 2, 1, 1, 1, 2, 2, 4 ),
 ( 0.000000000000000000, 0.1249999999999887590, 0.1874999999999831246, 0.2187499999999802380, 0.2343749999999805433, 0.2499999999999807931, 0.4999999999999914513, 0.6249999999999968914, 0.6875000000000003331, 0.7187500000000021094, 0.7343750000000029976, 0.7500000000000038858, 1.000000000000000000 ),
 .UNSPECIFIED. ) ;
#4759=CARTESIAN_POINT ( 'NONE',  ( 0.9176177226984534308, -3.499836378223736943, 230.7680100055947037 ) ) ;
#4896=FACE_OUTER_BOUND ( 'NONE', #14984, .T. ) ;
#4951=CARTESIAN_POINT ( 'NONE',  ( 0.000000000000000000, 0.000000000000000000, 230.8412452700000017 ) ) ;
#4959=AXIS2_PLACEMENT_3D ( 'NONE', #30406, #18430, #23320 ) ;
#4981=CARTESIAN_POINT ( 'NONE',  ( 1.747572776708516740, 1.007237960741798055, 227.6412452701233633 ) ) ;
#5115=CYLINDRICAL_SURFACE ( 'NONE', #25061, 2.000000000000000000 ) ;
#5133=CARTESIAN_POINT ( 'NONE',  ( 4.041451884329999800, 2.220446049249999755E-16, 230.8412452700000017 ) ) ;
#5184=CARTESIAN_POINT ( 'NONE',  ( 2.605043309139144281, 2.487932632647766873, 227.7052921205562370 ) ) ;
#5209=EDGE_CURVE ( 'NONE', #20042, #24964, #25845, .T. ) ;
#5278=UNCERTAINTY_MEASURE_WITH_UNIT (LENGTH_MEASURE( 1.000000000000000082E-05 ), #18011, 'distance_accuracy_value', 'NONE');
#5322=CARTESIAN_POINT ( 'NONE',  ( 380005.9281980000087, 207598.1847299999790, -249768.1509097300004 ) ) ;
#5366=CARTESIAN_POINT ( 'NONE',  ( 0.1574870170986610307, -3.500159137052063496, 230.8361063485508566 ) ) ;
#5481=B_SPLINE_CURVE_WITH_KNOTS ( 'NONE', 3,
 ( #9111, #6756, #10866, #20451, #4398, #6444, #11017, #1267, #1582, #4247, #18233, #20765, #25659, #30373, #4089, #13687, #13846, #28310, #18559, #23290, #6128, #23456, #20928, #22978, #1735, #16353 ),
 .UNSPECIFIED., .F., .F.,
 ( 4, 2, 2, 1, 1, 2, 2, 2, 2, 2, 1, 1, 2, 2, 4 ),
 ( 0.000000000000000000, 0.1249999999999754086, 0.1874999999999651112, 0.2187499999999598377, 0.2343749999999587830, 0.2421874999999582556, 0.2499999999999577560, 0.4999999999999693578, 0.6249999999999750200, 0.6874999999999777955, 0.7187499999999790168, 0.7343749999999812372, 0.7421874999999835687, 0.7499999999999859002, 1.000000000000000000 ),
 .UNSPECIFIED. ) ;
#5575=CARTESIAN_POINT ( 'NONE',  ( -2.449212707639999657E-16, 2.000000000000000000, 230.8412452696274499 ) ) ;
#5606=ORIENTED_EDGE ( 'NONE', *, *, #23406, .T. ) ;
#5684=ADVANCED_FACE ( 'NONE', ( #20072 ), #27447, .F. ) ;
#5693=CIRCLE ( 'NONE', #4715, 2.000000000000000000 ) ;
#5719=ORIENTED_EDGE ( 'NONE', *, *, #24701, .F. ) ;
#5803=ORIENTED_EDGE ( 'NONE', *, *, #412, .T. ) ;
#5841=CARTESIAN_POINT ( 'NONE',  ( 2.020725942159999899, 3.500000000000000000, 230.8412452700000017 ) ) ;
#5904=( LENGTH_UNIT ( ) NAMED_UNIT ( * ) SI_UNIT ( .MILLI., .METRE. ) );
#5962=CARTESIAN_POINT ( 'NONE',  ( -4.041451884379999804, 9.156941871420000667E-11, 227.9588918784999976 ) ) ;
#5975=CARTESIAN_POINT ( 'NONE',  ( 4.041451884379999804, -9.156941871420000667E-11, 229.2412452703699728 ) ) ;
#5984=CARTESIAN_POINT ( 'NONE',  ( -1.086409579022823424, -3.500000000000000000, 227.7407790647054071 ) ) ;
#6084=CARTESIAN_POINT ( 'NONE',  ( -3.072394438959999974, -1.678456730820000020, 230.8356432492296619 ) ) ;
#6107=VECTOR ( 'NONE', #372, 1000.000000000000000 ) ;
#6128=CARTESIAN_POINT ( 'NONE',  ( -2.582034095436241738, 2.527463138869748160, 227.7116136946786753 ) ) ;
#6136=CARTESIAN_POINT ( 'NONE',  ( 2.788509597084857461, 2.169696472159977851, 230.8175759419343365 ) ) ;
#6138=CARTESIAN_POINT ( 'NONE',  ( 0.7993620173054750699, -3.500000000000000000, 227.6978496355018251 ) ) ;
#6139=CARTESIAN_POINT ( 'NONE',  ( 3.072394438959999974, 1.678456730820000020, 227.6468472915199754 ) ) ;
#6145=ORIENTED_EDGE ( 'NONE', *, *, #23406, .F. ) ;
#6155=CARTESIAN_POINT ( 'NONE',  ( 2.116742336517584366, -3.333694726622333793, 227.9034567869041155 ) ) ;
#6177=EDGE_CURVE ( 'NONE', #2338, #27018, #1776, .T. ) ;
#6213=ORIENTED_EDGE ( 'NONE', *, *, #4502, .F. ) ;
#6251=CARTESIAN_POINT ( 'NONE',  ( -2.020725942269999909, -3.500000000000000000, 230.5235986622430175 ) ) ;
#6253=CARTESIAN_POINT ( 'NONE',  ( 0.000000000000000000, 0.000000000000000000, 227.6412452700500069 ) ) ;
#6283=CARTESIAN_POINT ( 'NONE',  ( 1.746192186286341652, -1.009653006786209506, 230.8412452700000301 ) ) ;
#6304=CARTESIAN_POINT ( 'NONE',  ( 2.020725942159999899, -3.500000000000000000, 227.9588918784999976 ) ) ;
#6352=EDGE_CURVE ( 'NONE', #53, #15258, #5481, .T. ) ;
#6395=CARTESIAN_POINT ( 'NONE',  ( -3.858789587622685868, -0.3163803785149745251, 230.6290587881455849 ) ) ;
#6410=DIRECTION ( 'NONE',  ( 0.000000000000000000, 0.000000000000000000, -1.000000000000000000 ) ) ;
#6435=CARTESIAN_POINT ( 'NONE',  ( 2.000067258429029771, -0.2648802556752501425, 230.8412452700000301 ) ) ;
#6444=CARTESIAN_POINT ( 'NONE',  ( -3.610091233028032587, 0.7466883238378643206, 227.7538236713938602 ) ) ;
#6453=CARTESIAN_POINT ( 'NONE',  ( -0.6215321086153002828, -3.499999999999999556, 227.6701688388543516 ) ) ;
#6501=CARTESIAN_POINT ( 'NONE',  ( 4.041451884329999800, 2.701186720849999812E-16, 227.9588918784999976 ) ) ;
#6509=CARTESIAN_POINT ( 'NONE',  ( 0.000000000000000000, 0.000000000000000000, 230.8412452696274499 ) ) ;
#6623=ADVANCED_FACE ( 'NONE', ( #13074 ), #17790, .T. ) ;
#6634=CARTESIAN_POINT ( 'NONE',  ( -1.833239707770263127, 3.499999999998122391, 227.9047692640812670 ) ) ;
#6711=CARTESIAN_POINT ( 'NONE',  ( -2.748065355775931806, -2.239845275112382961, 230.8106057538883249 ) ) ;
#6756=CARTESIAN_POINT ( 'NONE',  ( -3.947708767128641938, 0.1623678418503206877, 227.9047692640809544 ) ) ;
#6763=CARTESIAN_POINT ( 'NONE',  ( 2.590102362141937675, 2.513801395321815679, 230.7730491447829877 ) ) ;
#6786=CARTESIAN_POINT ( 'NONE',  ( 3.361916939940001292, -1.176989049201372595, 227.6811464142205068 ) ) ;
#6794=CARTESIAN_POINT ( 'NONE',  ( -1.291648043291917070, 3.499742528936139241, 227.7788113689714464 ) ) ;
#6857=CARTESIAN_POINT ( 'NONE',  ( -4.041451884379999804, 9.156941871420000667E-11, 230.5235986622430175 ) ) ;
#6872=CARTESIAN_POINT ( 'NONE',  ( 2.385041915132713353, -2.868471282680012724, 230.7036791710386296 ) ) ;
#6948=CARTESIAN_POINT ( 'NONE',  ( 0.9263908148288600986, 3.499834818475870968, 227.7157682482504413 ) ) ;
#7104=EDGE_CURVE ( 'NONE', #7731, #11038, #13786, .T. ) ;
#7112=CARTESIAN_POINT ( 'NONE',  ( -2.020725942269999909, -3.500000000000000000, 230.5235986622430175 ) ) ;
#7230=DIRECTION ( 'NONE',  ( 0.000000000000000000, 0.000000000000000000, -1.000000000000000000 ) ) ;
#7284=EDGE_CURVE ( 'NONE', #9026, #11038, #16554, .T. ) ;
#7429=EDGE_LOOP ( 'NONE', ( #1438, #5803 ) ) ;
#7524=CARTESIAN_POINT ( 'NONE',  ( 1.636264169893193676, 3.500000000000000000, 230.6345832158283145 ) ) ;
#7534=CARTESIAN_POINT ( 'NONE',  ( 0.000000000000000000, 0.000000000000000000, 227.6412452703700069 ) ) ;
#7557=CARTESIAN_POINT ( 'NONE',  ( 0.000000000000000000, 0.000000000000000000, 227.6412452700500069 ) ) ;
#7628=CARTESIAN_POINT ( 'NONE',  ( 3.511914029064534315, 0.9171864698412210970, 230.7613442533399279 ) ) ;
#7697=CARTESIAN_POINT ( 'NONE',  ( 2.728640529172922768, 2.273855967875096695, 227.6754430268697718 ) ) ;
#7719=CARTESIAN_POINT ( 'NONE',  ( 0.8978302376563351839, -3.499838689521491464, 230.7708768453263701 ) ) ;
#7731=VERTEX_POINT ( 'NONE', #10119 ) ;
#7759=ORIENTED_EDGE ( 'NONE', *, *, #12733, .F. ) ;
#7851=B_SPLINE_CURVE_WITH_KNOTS ( 'NONE', 3,
 ( #22432, #12361, #726, #21970, #424, #10006, #19913, #10473, #29659, #17680, #27296, #15644, #11244 ),
 .UNSPECIFIED., .F., .F.,
 ( 4, 2, 2, 1, 2, 2, 4 ),
 ( 0.000000000000000000, 0.2500000000000028866, 0.3750000000000024980, 0.4375000000000026090, 0.4687500000000026645, 0.5000000000000027756, 1.000000000000000000 ),
 .UNSPECIFIED. ) ;
#7863=CARTESIAN_POINT ( 'NONE',  ( -2.625702655398183261, -2.452149595275970206, 227.6997972603546998 ) ) ;
#8158=CARTESIAN_POINT ( 'NONE',  ( -3.427383197786517677, -1.063472793697235241, 227.6973195743569249 ) ) ;
#8174=CARTESIAN_POINT ( 'NONE',  ( 2.687036963354079155, 2.345727656310530485, 230.7977248921758928 ) ) ;
#8260=SURFACE_STYLE_FILL_AREA ( #27008 ) ;
#8314=CARTESIAN_POINT ( 'NONE',  ( -3.503090509784088091, -0.9324612817112352126, 227.7184664424322591 ) ) ;
#8337=ORIENTED_EDGE ( 'NONE', *, *, #28321, .T. ) ;
#8369=ORIENTED_EDGE ( 'NONE', *, *, #6177, .F. ) ;
#8406=EDGE_CURVE ( 'NONE', #11038, #9026, #29002, .T. ) ;
#8412=SHAPE_REPRESENTATION_RELATIONSHIP ( 'NONE' , 'NONE' ,  #339, #14437 ) ;
#8416=ORIENTED_EDGE ( 'NONE', *, *, #11545, .T. ) ;
#8434=CARTESIAN_POINT ( 'NONE',  ( -2.601833019719681950, 2.493493017038428405, 230.7766559207227601 ) ) ;
#8470=CARTESIAN_POINT ( 'NONE',  ( -3.691781163152999312, -0.6055607618816524207, 227.7772386881452462 ) ) ;
#8476=CONICAL_SURFACE ( 'NONE', #21555, 3.491271820449999286, 1.047197551199999799 ) ;
#8482=LINE ( 'NONE', #5975, #25817 ) ;
#8490=CARTESIAN_POINT ( 'NONE',  ( -1.549220603345442315, -3.499999999999999556, 227.8316576175188857 ) ) ;
#8518=AXIS2_PLACEMENT_3D ( 'NONE', #5841, #15443, #3476 ) ;
#8534=VERTEX_POINT ( 'NONE', #11591 ) ;
#8585=DIRECTION ( 'NONE',  ( 0.000000000000000000, 0.000000000000000000, -1.000000000000000000 ) ) ;
#8586=CARTESIAN_POINT ( 'NONE',  ( -3.503013490857829204, -0.9326026542299333810, 230.7640337244225464 ) ) ;
#8595=CARTESIAN_POINT ( 'NONE',  ( -3.574293702744737455, 0.8091417056767529203, 230.7417114753004341 ) ) ;
#8604=CARTESIAN_POINT ( 'NONE',  ( 3.676328827952111578, -0.6318780627718988407, 230.7123227554324956 ) ) ;
#8631=MECHANICAL_DESIGN_GEOMETRIC_PRESENTATION_REPRESENTATION('',(#22222),#15178);
#8640=CARTESIAN_POINT ( 'NONE',  ( 2.020725942159999899, -3.500000000000000000, 227.9588918784999976 ) ) ;
#8650=VERTEX_POINT ( 'NONE', #6857 ) ;
#8698=VECTOR ( 'NONE', #1465, 1000.000000000000000 ) ;
#8832=CARTESIAN_POINT ( 'NONE',  ( -0.9592076359739227787, 3.499847752373102860, 227.7207037332364052 ) ) ;
#8835=B_SPLINE_CURVE_WITH_KNOTS ( 'NONE', 3,
 ( #20559, #27955, #21036, #23408, #25607, #3560, #8586, #25449, #3882, #6395, #15994 ),
 .UNSPECIFIED., .F., .F.,
 ( 4, 1, 1, 1, 2, 2, 4 ),
 ( 0.000000000000000000, 0.2500000000000179301, 0.3750000000000248690, 0.4375000000000283662, 0.4687500000000269229, 0.5000000000000254241, 1.000000000000000000 ),
 .UNSPECIFIED. ) ;
#8916=CARTESIAN_POINT ( 'NONE',  ( -2.212956828297914846, 3.167046338434466257, 230.6345832158275186 ) ) ;
#8942=DIRECTION ( 'NONE',  ( 0.000000000000000000, -1.000000000000000000, 0.000000000000000000 ) ) ;
#8994=CARTESIAN_POINT ( 'NONE',  ( 0.9176177227138302417, 3.499836378220442690, 227.7144805344090059 ) ) ;
#9012=ORIENTED_EDGE ( 'NONE', *, *, #25988, .F. ) ;
#9025=PLANE ( 'NONE',  #3515 ) ;
#9026=VERTEX_POINT ( 'NONE', #14098 ) ;
#9083=CARTESIAN_POINT ( 'NONE',  ( 2.523699655483016446, -2.628482120109524089, 230.7531903453053133 ) ) ;
#9111=CARTESIAN_POINT ( 'NONE',  ( -4.041451884379999804, 9.156941871420000667E-11, 227.9588918784999976 ) ) ;
#9135=CARTESIAN_POINT ( 'NONE',  ( 3.668680263715867973, -0.6456593865231384788, 227.7673180537741473 ) ) ;
#9172=DIRECTION ( 'NONE',  ( 0.000000000000000000, 0.000000000000000000, -1.000000000000000000 ) ) ;
#9232=CARTESIAN_POINT ( 'NONE',  ( 2.020725942159999899, -3.500000000000000000, 230.5235986622430175 ) ) ;
#9270=CARTESIAN_POINT ( 'NONE',  ( 2.020725942159999899, 3.500000000000000000, 230.5235986622430175 ) ) ;
#9382=CARTESIAN_POINT ( 'NONE',  ( 0.000000000000000000, -2.000000000000000000, 227.6412452703700069 ) ) ;
#9537=CARTESIAN_POINT ( 'NONE',  ( 3.455337460958629148, 1.015179960318480346, 230.7778176299132156 ) ) ;
#9581=CARTESIAN_POINT ( 'NONE',  ( 0.3874847876386515733, 3.500000000000000000, 230.8270369382009051 ) ) ;
#9593=CARTESIAN_POINT ( 'NONE',  ( -380005.9281980000087, -207598.1847299999790, -249768.1509097300004 ) ) ;
#9624=CARTESIAN_POINT ( 'NONE',  ( -1.380865576384323168, -3.499743769985608211, 230.6852868990059164 ) ) ;
#9630=ORIENTED_EDGE ( 'NONE', *, *, #2965, .T. ) ;
#9700=CARTESIAN_POINT ( 'NONE',  ( 2.000000000000000000, 0.2617993877991477425, 227.6412452701696054 ) ) ;
#9717=FILL_AREA_STYLE ('',( #24507 ) ) ;
#9729=CARTESIAN_POINT ( 'NONE',  ( 0.8585117870366192339, 3.500000000000000000, 230.7766559207250339 ) ) ;
#9758=CARTESIAN_POINT ( 'NONE',  ( 2.407487872917116967, 2.830108685495575926, 227.7614631413372308 ) ) ;
#9790=ORIENTED_EDGE ( 'NONE', *, *, #12733, .T. ) ;
#9840=EDGE_CURVE ( 'NONE', #22953, #15258, #11501, .T. ) ;
#9919=CARTESIAN_POINT ( 'NONE',  ( 2.595403069823767339, 2.504630016939114689, 227.7079405341281699 ) ) ;
#9939=CARTESIAN_POINT ( 'NONE',  ( 0.7992118187927096384, -3.499831230572010288, 230.7844944799418272 ) ) ;
#9956=LINE ( 'NONE', #25044, #6107 ) ;
#10006=CARTESIAN_POINT ( 'NONE',  ( 3.427383197809986903, 1.063472793664595129, 227.6973195743642862 ) ) ;
#10037=SURFACE_STYLE_USAGE ( .BOTH. , #28753 ) ;
#10039=LINE ( 'NONE', #2799, #26025 ) ;
#10050=VECTOR ( 'NONE', #16454, 1000.000000000000227 ) ;
#10074=EDGE_LOOP ( 'NONE', ( #10414, #16705, #10845, #17438, #448, #18215 ) ) ;
#10096=CARTESIAN_POINT ( 'NONE',  ( -1.833239707743530955, -3.500000000000507594, 230.5777212759286670 ) ) ;
#10119=CARTESIAN_POINT ( 'NONE',  ( -3.072394438959999974, -1.678456730820000020, 227.6468472915199754 ) ) ;
#10252=ORIENTED_EDGE ( 'NONE', *, *, #25988, .T. ) ;
#10414=ORIENTED_EDGE ( 'NONE', *, *, #25796, .F. ) ;
#10456=ORIENTED_EDGE ( 'NONE', *, *, #5209, .T. ) ;
#10473=CARTESIAN_POINT ( 'NONE',  ( 3.484101657956257370, 0.9653352590934711763, 227.7128614111574052 ) ) ;
#10495=CONICAL_SURFACE ( 'NONE', #2970, 3.491271820449999286, 1.047197551199999799 ) ;
#10566=EDGE_LOOP ( 'NONE', ( #6145, #30696, #8416, #14112, #206, #10879, #30148 ) ) ;
#10612=PLANE ( 'NONE',  #28561 ) ;
#10686=CARTESIAN_POINT ( 'NONE',  ( 3.072394438959999974, 1.678456730820000020, 230.8356432492296619 ) ) ;
#10689=CARTESIAN_POINT ( 'NONE',  ( 1.601115582524632597, -1.226324675095826988, 230.8412452700000301 ) ) ;
#10821=CARTESIAN_POINT ( 'NONE',  ( -2.020725942109999895, 3.500000000090000007, 230.5235986622430175 ) ) ;
#10845=ORIENTED_EDGE ( 'NONE', *, *, #29319, .T. ) ;
#10854=CARTESIAN_POINT ( 'NONE',  ( 1.226324675095736394, 1.601115582524161862, 230.8412452700000017 ) ) ;
#10866=CARTESIAN_POINT ( 'NONE',  ( -3.856237990133467353, 0.3204508335913280881, 227.8575818780809357 ) ) ;
#10879=ORIENTED_EDGE ( 'NONE', *, *, #25796, .T. ) ;
#10974=EDGE_CURVE ( 'NONE', #31001, #9026, #28295, .T. ) ;
#10975=CARTESIAN_POINT ( 'NONE',  ( -3.945435489976578225, 0.1663052733796139271, 230.5790337530978036 ) ) ;
#11017=CARTESIAN_POINT ( 'NONE',  ( -3.576869721619468478, 0.8042774860780150803, 227.7419800002267039 ) ) ;
#11038=VERTEX_POINT ( 'NONE', #16642 ) ;
#11043=CARTESIAN_POINT ( 'NONE',  ( -4.041451884379999804, 9.156941871420000667E-11, 227.9588918784999976 ) ) ;
#11131=CARTESIAN_POINT ( 'NONE',  ( -3.520849940866991989, 0.9017090165965767623, 230.7589734104482488 ) ) ;
#11138=EDGE_CURVE ( 'NONE', #18457, #29946, #10039, .T. ) ;
#11148=ORIENTED_EDGE ( 'NONE', *, *, #6177, .T. ) ;
#11177=CARTESIAN_POINT ( 'NONE',  ( -0.9795220552721649598, -3.499999999999999556, 227.7235171295581893 ) ) ;
#11196=FACE_OUTER_BOUND ( 'NONE', #13662, .T. ) ;
#11203=CARTESIAN_POINT ( 'NONE',  ( -0.9813161448799405662, 3.499840617129988285, 227.7241098089419893 ) ) ;
#11244=CARTESIAN_POINT ( 'NONE',  ( 4.041451884329999800, 2.701186720849999812E-16, 227.9588918784999976 ) ) ;
#11262=AXIS2_PLACEMENT_3D ( 'NONE', #21070, #28291, #8942 ) ;
#11290=CARTESIAN_POINT ( 'NONE',  ( -3.509522867613010355, 0.9213280829735164268, 230.7624477058855632 ) ) ;
#11296=CARTESIAN_POINT ( 'NONE',  ( -0.6215321085541587465, 3.500000000000000000, 230.8123217011518022 ) ) ;
#11306=EDGE_CURVE ( 'NONE', #28246, #8650, #8835, .T. ) ;
#11364=CARTESIAN_POINT ( 'NONE',  ( -0.3140692933633429940, 3.500175508921068435, 227.6463701859492517 ) ) ;
#11393=DIRECTION ( 'NONE',  ( 0.000000000000000000, -1.000000000000000000, 0.000000000000000000 ) ) ;
#11445=CARTESIAN_POINT ( 'NONE',  ( -2.572901307054817011, 2.543604213323934271, 230.7685035973561583 ) ) ;
#11501=LINE ( 'NONE', #18420, #18490 ) ;
#11545=EDGE_CURVE ( 'NONE', #28246, #8534, #27737, .T. ) ;
#11551=DIRECTION ( 'NONE',  ( 0.000000000000000000, -1.000000000000000000, 0.000000000000000000 ) ) ;
#11591=CARTESIAN_POINT ( 'NONE',  ( -3.063879268240000009, -1.673804873600000187, 230.8412452700000017 ) ) ;
#11602=CARTESIAN_POINT ( 'NONE',  ( 0.5234957687185606279, 1.947945353336631324, 227.6412452700308791 ) ) ;
#11608=CARTESIAN_POINT ( 'NONE',  ( 2.721155027367574863, -2.286694320792284962, 230.8124538892466262 ) ) ;
#11709=VERTEX_POINT ( 'NONE', #30356 ) ;
#11753=CARTESIAN_POINT ( 'NONE',  ( 1.229093439949827005, -1.599333684796362176, 227.6412452702929841 ) ) ;
#11774=( LENGTH_UNIT ( ) NAMED_UNIT ( * ) SI_UNIT ( .MILLI., .METRE. ) );
#11788=DIRECTION ( 'NONE',  ( 0.000000000000000000, 0.000000000000000000, -1.000000000000000000 ) ) ;
#11893=CARTESIAN_POINT ( 'NONE',  ( 3.072394438959999974, 1.678456730820000020, 230.8356432492296619 ) ) ;
#11958=EDGE_CURVE ( 'NONE', #18690, #29368, #24816, .T. ) ;
#11965=CARTESIAN_POINT ( 'NONE',  ( 2.625702655411691566, 2.452149595252573366, 227.6997972603473386 ) ) ;
#11984=CARTESIAN_POINT ( 'NONE',  ( 0.5453808542213991473, -3.499787565727024763, 230.8124249489340230 ) ) ;
#11994=B_SPLINE_CURVE_WITH_KNOTS ( 'NONE', 3,
 ( #6084, #25770, #23250, #15682, #6711, #21046, #25293, #4201, #27802, #3729, #30646, #13802, #22937, #6251 ),
 .UNSPECIFIED., .F., .F.,
 ( 4, 2, 2, 1, 1, 2, 2, 4 ),
 ( 0.000000000000000000, 0.2499999999999499845, 0.3749999999999247269, 0.4374999999999122924, 0.4687499999999084621, 0.4843749999999067413, 0.4999999999999050759, 1.000000000000000000 ),
 .UNSPECIFIED. ) ;
#12074=ORIENTED_EDGE ( 'NONE', *, *, #7284, .T. ) ;
#12136=CARTESIAN_POINT ( 'NONE',  ( -1.650600432482589808, -3.499825479288129593, 230.6249086619309310 ) ) ;
#12243=CARTESIAN_POINT ( 'NONE',  ( 0.6616560533698909730, 3.499999999999999112, 230.8013441257845102 ) ) ;
#12254=AXIS2_PLACEMENT_3D ( 'NONE', #5133, #14746, #24343 ) ;
#12361=CARTESIAN_POINT ( 'NONE',  ( 3.147559148823465769, 1.548267634410576132, 227.6488953029178219 ) ) ;
#12390=DIRECTION ( 'NONE',  ( 0.000000000000000000, 0.000000000000000000, -1.000000000000000000 ) ) ;
#12439=ADVANCED_FACE ( 'NONE', ( #11196 ), #20797, .T. ) ;
#12474=CARTESIAN_POINT ( 'NONE',  ( -8.881784197000000993E-16, 2.220446049249999755E-16, 230.8412452700000017 ) ) ;
#12504=UNCERTAINTY_MEASURE_WITH_UNIT (LENGTH_MEASURE( 1.000000000000000082E-05 ), #5904, 'distance_accuracy_value', 'NONE');
#12585=ORIENTED_EDGE ( 'NONE', *, *, #7104, .T. ) ;
#12599=CARTESIAN_POINT ( 'NONE',  ( 1.645798001284060064, -3.500000000000228706, 230.6318310357691814 ) ) ;
#12627=CARTESIAN_POINT ( 'NONE',  ( -4.041451884329999800, 1.776356839399999804E-15, 230.8412452700000017 ) ) ;
#12673=EDGE_CURVE ( 'NONE', #7731, #53, #24173, .T. ) ;
#12680=( NAMED_UNIT ( * ) SI_UNIT ( $, .STERADIAN. ) SOLID_ANGLE_UNIT ( ) );
#12724=AXIS2_PLACEMENT_3D ( 'NONE', #12627, #696, #19884 ) ;
#12733=EDGE_CURVE ( 'NONE', #18457, #26221, #30595, .T. ) ;
#12746=CARTESIAN_POINT ( 'NONE',  ( -2.871635305848837305, -2.026181749455575609, 227.6510696331287420 ) ) ;
#12758=ORIENTED_EDGE ( 'NONE', *, *, #8406, .T. ) ;
#12862=ORIENTED_EDGE ( 'NONE', *, *, #20435, .F. ) ;
#12867=LINE ( 'NONE', #5322, #23064 ) ;
#13046=CARTESIAN_POINT ( 'NONE',  ( -3.072394438959999974, -1.678456730820000020, 227.6468472915199754 ) ) ;
#13074=FACE_OUTER_BOUND ( 'NONE', #10074, .T. ) ;
#13208=CIRCLE ( 'NONE', #13292, 3.491271820589999741 ) ;
#13211=CARTESIAN_POINT ( 'NONE',  ( 2.656431219450670067, 2.398832595345626650, 230.7906780664011706 ) ) ;
#13213=( GEOMETRIC_REPRESENTATION_CONTEXT ( 3 ) GLOBAL_UNCERTAINTY_ASSIGNED_CONTEXT ( ( #12504 ) ) GLOBAL_UNIT_ASSIGNED_CONTEXT ( ( #5904, #3547, #24803 ) ) REPRESENTATION_CONTEXT ( 'NONE', 'WORKASPACE' ) );
#13292=AXIS2_PLACEMENT_3D ( 'NONE', #12474, #26648, #23992 ) ;
#13295=ADVANCED_FACE ( 'NONE', ( #19445 ), #5115, .F. ) ;
#13333=PLANE ( 'NONE',  #1065 ) ;
#13337=PRODUCT_DEFINITION_SHAPE ( 'NONE', 'NONE',  #2325 ) ;
#13394=CARTESIAN_POINT ( 'NONE',  ( 3.489276519439490798, -0.9563957866777589301, 227.7139869426456471 ) ) ;
#13433=DIRECTION ( 'NONE',  ( 0.000000000000000000, 0.000000000000000000, -1.000000000000000000 ) ) ;
#13485=DIRECTION ( 'NONE',  ( -0.8775825618903722036, -0.4794255386042040601, 0.000000000000000000 ) ) ;
#13504=SHAPE_DEFINITION_REPRESENTATION ( #13337, #339 ) ;
#13517=CARTESIAN_POINT ( 'NONE',  ( -8.424250880209998925E-16, -2.000000000000000000, 230.8412452700000017 ) ) ;
#13536=CARTESIAN_POINT ( 'NONE',  ( 0.6616560533897080099, -3.500000000000000444, 227.6811464142208479 ) ) ;
#13552=CLOSED_SHELL ( 'NONE', ( #26530, #995, #28156, #19886, #6623, #12439, #14010, #29468, #14404, #20556, #26844, #15389, #13295, #5684 ) ) ;
#13558=CARTESIAN_POINT ( 'NONE',  ( 2.720322858944644207, -2.288262595320229131, 227.6701688388524190 ) ) ;
#13600=FACE_OUTER_BOUND ( 'NONE', #29253, .T. ) ;
#13645=CARTESIAN_POINT ( 'NONE',  ( -2.631407904598755287, 2.442267813799901433, 230.7846409045018277 ) ) ;
#13662=EDGE_LOOP ( 'NONE', ( #3986, #30581, #3317, #22452 ) ) ;
#13687=CARTESIAN_POINT ( 'NONE',  ( -2.758214512664866280, 2.222207457346479842, 227.6700655910688056 ) ) ;
#13720=CARTESIAN_POINT ( 'NONE',  ( 0.5453808542172137175, 3.499787565727434213, 227.6700655910692603 ) ) ;
#13786=LINE ( 'NONE', #18969, #10050 ) ;
#13802=CARTESIAN_POINT ( 'NONE',  ( -2.400053023227272764, -2.842866040671395922, 230.7188131565800404 ) ) ;
#13846=CARTESIAN_POINT ( 'NONE',  ( -2.719334904039233169, 2.289552478158404902, 227.6774647154331319 ) ) ;
#13874=CARTESIAN_POINT ( 'NONE',  ( 2.487884123742928111, -2.690858294336446743, 227.7407790647027923 ) ) ;
#14000=CARTESIAN_POINT ( 'NONE',  ( 0.1546076948784753102, 3.500000000000000000, 230.8358359828806954 ) ) ;
#14010=ADVANCED_FACE ( 'NONE', ( #15763 ), #10495, .T. ) ;
#14015=DIRECTION ( 'NONE',  ( 0.000000000000000000, 0.000000000000000000, 1.000000000000000000 ) ) ;
#14098=CARTESIAN_POINT ( 'NONE',  ( 3.063879268240000009, 1.673804873600000187, 227.6412452699999847 ) ) ;
#14101=EDGE_CURVE ( 'NONE', #18566, #27661, #12867, .T. ) ;
#14112=ORIENTED_EDGE ( 'NONE', *, *, #412, .F. ) ;
#14201=ORIENTED_EDGE ( 'NONE', *, *, #6352, .F. ) ;
#14205=CARTESIAN_POINT ( 'NONE',  ( -2.020725942109999895, 3.500000000090000007, 230.5235986622430175 ) ) ;
#14343=CARTESIAN_POINT ( 'NONE',  ( 3.072394438959999974, 1.678456730820000020, 227.6468472915199754 ) ) ;
#14404=ADVANCED_FACE ( 'NONE', ( #22627 ), #8476, .T. ) ;
#14437=ADVANCED_BREP_SHAPE_REPRESENTATION ( '', ( #540, #17722 ), #14741 ) ;
#14522=ORIENTED_EDGE ( 'NONE', *, *, #24701, .T. ) ;
#14642=CONICAL_SURFACE ( 'NONE', #3546, 3.491271820449999286, 1.047197551199999799 ) ;
#14726=DIRECTION ( 'NONE',  ( 0.000000000000000000, -1.000000000000000000, 0.000000000000000000 ) ) ;
#14741=( GEOMETRIC_REPRESENTATION_CONTEXT ( 3 ) GLOBAL_UNCERTAINTY_ASSIGNED_CONTEXT ( ( #5278 ) ) GLOBAL_UNIT_ASSIGNED_CONTEXT ( ( #18011, #24957, #12680 ) ) REPRESENTATION_CONTEXT ( 'NONE', 'WORKASPACE' ) );
#14746=DIRECTION ( 'NONE',  ( 0.8660254037843290176, -0.5000000000001900702, 0.000000000000000000 ) ) ;
#14797=CARTESIAN_POINT ( 'NONE',  ( 2.219613442066579623, 3.155516745171627058, 227.8440641264181750 ) ) ;
#14885=CARTESIAN_POINT ( 'NONE',  ( 3.257018533420329653, 1.358678418917213637, 230.8224594091670383 ) ) ;
#14898=CARTESIAN_POINT ( 'NONE',  ( 2.020725942159999899, -3.500000000000000000, 230.5235986622430175 ) ) ;
#14931=FACE_OUTER_BOUND ( 'NONE', #21288, .T. ) ;
#14973=CARTESIAN_POINT ( 'NONE',  ( 0.9263908148115145291, -3.499834818479312659, 230.7667222917537515 ) ) ;
#14984=EDGE_LOOP ( 'NONE', ( #8337, #19527, #3245, #12074, #29601, #16335, #19960 ) ) ;
#15006=B_SPLINE_CURVE_WITH_KNOTS ( 'NONE', 3,
 ( #18245, #15431, #8490, #3943, #5984, #17926, #11177, #25186, #6453, #30383, #1745, #3619, #13536, #6138, #20776, #22827, #23147, #1590, #22987, #6304 ),
 .UNSPECIFIED., .F., .F.,
 ( 4, 1, 1, 1, 2, 2, 2, 1, 1, 1, 2, 2, 4 ),
 ( 0.000000000000000000, 0.1250000000000261458, 0.1875000000000392186, 0.2187500000000439648, 0.2343750000000447697, 0.2500000000000455747, 0.5000000000000199840, 0.6250000000000072164, 0.6875000000000016653, 0.7187500000000001110, 0.7343749999999980016, 0.7499999999999957812, 1.000000000000000000 ),
 .UNSPECIFIED. ) ;
#15122=ORIENTED_EDGE ( 'NONE', *, *, #23460, .F. ) ;
#15178=( GEOMETRIC_REPRESENTATION_CONTEXT ( 3 ) GLOBAL_UNCERTAINTY_ASSIGNED_CONTEXT ( ( #21037 ) ) GLOBAL_UNIT_ASSIGNED_CONTEXT ( ( #11774, #23906, #16797 ) ) REPRESENTATION_CONTEXT ( 'NONE', 'WORKASPACE' ) );
#15246=ORIENTED_EDGE ( 'NONE', *, *, #20014, .T. ) ;
#15258=VERTEX_POINT ( 'NONE', #2679 ) ;
#15264=CARTESIAN_POINT ( 'NONE',  ( -2.020725942269999909, -3.500000000000000000, 227.9588918784999976 ) ) ;
#15336=DIRECTION ( 'NONE',  ( 0.000000000000000000, -1.000000000000000000, 0.000000000000000000 ) ) ;
#15389=ADVANCED_FACE ( 'NONE', ( #29653, #13600 ), #10612, .T. ) ;
#15410=CARTESIAN_POINT ( 'NONE',  ( -3.370970677383902103, -1.161062029692211173, 227.6835602974589108 ) ) ;
#15431=CARTESIAN_POINT ( 'NONE',  ( -1.828693153458612164, -3.500000000000001332, 227.9034567869048544 ) ) ;
#15443=DIRECTION ( 'NONE',  ( 0.8660254037843290176, 0.5000000000001900702, -0.000000000000000000 ) ) ;
#15564=CARTESIAN_POINT ( 'NONE',  ( -2.407487872911075577, -2.830108685506040000, 227.7614631413448762 ) ) ;
#15644=CARTESIAN_POINT ( 'NONE',  ( 3.862245930686361461, 0.3103938167200858689, 227.8554272724557279 ) ) ;
#15682=CARTESIAN_POINT ( 'NONE',  ( -2.788509597074717572, -2.169696472188583858, 230.8175759419288795 ) ) ;
#15705=DIRECTION ( 'NONE',  ( -0.7600087925169251024, -0.4151946956549595336, -0.4999999999969509945 ) ) ;
#15712=CARTESIAN_POINT ( 'NONE',  ( -3.333579493018210105, -1.225759174659744932, 227.6757455870635454 ) ) ;
#15732=CARTESIAN_POINT ( 'NONE',  ( 2.620483857039677567, 2.461162703741023527, 230.7813955785624387 ) ) ;
#15753=CARTESIAN_POINT ( 'NONE',  ( 2.411999711991697382, -2.822293950991988432, 227.7677604876778332 ) ) ;
#15763=FACE_OUTER_BOUND ( 'NONE', #10566, .T. ) ;
#15777=EDGE_LOOP ( 'NONE', ( #10252, #25453, #2289, #15801 ) ) ;
#15788=ORIENTED_EDGE ( 'NONE', *, *, #29319, .F. ) ;
#15796=CARTESIAN_POINT ( 'NONE',  ( 0.000000000000000000, -2.000000000000000000, 227.6412452703700069 ) ) ;
#15801=ORIENTED_EDGE ( 'NONE', *, *, #2965, .F. ) ;
#15856=DIRECTION ( 'NONE',  ( 0.000000000000000000, 0.000000000000000000, 1.000000000000000000 ) ) ;
#15884=CARTESIAN_POINT ( 'NONE',  ( 1.226419552955990477, -1.601210460385421808, 230.8412452700000301 ) ) ;
#15898=CARTESIAN_POINT ( 'NONE',  ( 2.215775945524685486, 3.162163484153768689, 230.6362108339230588 ) ) ;
#15924=CARTESIAN_POINT ( 'NONE',  ( -1.650600432523903427, 3.499825479287930641, 227.8575818780827262 ) ) ;
#15994=CARTESIAN_POINT ( 'NONE',  ( -4.041451884379999804, 9.156941871420000667E-11, 230.5235986622430175 ) ) ;
#16014=CARTESIAN_POINT ( 'NONE',  ( 3.465040867608843556, -0.9980531523770136415, 230.7751077600194094 ) ) ;
#16019=ORIENTED_EDGE ( 'NONE', *, *, #9840, .T. ) ;
#16081=CARTESIAN_POINT ( 'NONE',  ( -1.014482461697403970, 3.499829073224391074, 227.7293001947028586 ) ) ;
#16148=DIRECTION ( 'NONE',  ( 0.000000000000000000, -1.000000000000000000, 0.000000000000000000 ) ) ;
#16232=CARTESIAN_POINT ( 'NONE',  ( 1.645798001274432654, 3.499999999995804689, 227.8506595042291565 ) ) ;
#16234=CARTESIAN_POINT ( 'NONE',  ( -2.020725942159999899, -3.500000000000000000, 229.2412452703699728 ) ) ;
#16254=EDGE_CURVE ( 'NONE', #31001, #27054, #7851, .T. ) ;
#16335=ORIENTED_EDGE ( 'NONE', *, *, #12673, .T. ) ;
#16353=CARTESIAN_POINT ( 'NONE',  ( -2.020725942109999895, 3.500000000090000007, 227.9588918784999976 ) ) ;
#16358=PRODUCT_DEFINITION_FORMATION_WITH_SPECIFIED_SOURCE ( 'ANY', '', #18097, .NOT_KNOWN. ) ;
#16391=CARTESIAN_POINT ( 'NONE',  ( -0.6197578588520477050, 3.499936541727148409, 227.6700366507586466 ) ) ;
#16454=DIRECTION ( 'NONE',  ( 0.7600087925169251024, 0.4151946956549595336, -0.4999999999969509945 ) ) ;
#16474=CARTESIAN_POINT ( 'NONE',  ( 3.187192794176077815, -1.479400473301520913, 230.8301842479609149 ) ) ;
#16554=CIRCLE ( 'NONE', #978, 3.491271820589999741 ) ;
#16642=CARTESIAN_POINT ( 'NONE',  ( -3.063879268240000009, -1.673804873600000187, 227.6412452699999847 ) ) ;
#16696=CARTESIAN_POINT ( 'NONE',  ( -1.014482461663960056, -3.499829073223180931, 230.7531903453067628 ) ) ;
#16705=ORIENTED_EDGE ( 'NONE', *, *, #4502, .T. ) ;
#16797=( NAMED_UNIT ( * ) SI_UNIT ( $, .STERADIAN. ) SOLID_ANGLE_UNIT ( ) );
#16965=CARTESIAN_POINT ( 'NONE',  ( -2.020725942109999895, 3.500000000090000007, 230.5235986622430175 ) ) ;
#17097=PLANE ( 'NONE',  #12254 ) ;
#17119=CARTESIAN_POINT ( 'NONE',  ( -1.238178402492337682, 3.499999999999999112, 230.7147300523246543 ) ) ;
#17317=CARTESIAN_POINT ( 'NONE',  ( -3.072394438959999974, -1.678456730820000020, 227.6468472915199754 ) ) ;
#17438=ORIENTED_EDGE ( 'NONE', *, *, #16254, .F. ) ;
#17466=CARTESIAN_POINT ( 'NONE',  ( -2.595403069806114793, -2.504630016969688011, 227.7079405341370091 ) ) ;
#17534=CARTESIAN_POINT ( 'NONE',  ( 4.041451884329999800, 2.220446049249999755E-16, 230.5235986622430175 ) ) ;
#17680=CARTESIAN_POINT ( 'NONE',  ( 3.511528848221511012, 0.9178490656560075456, 227.7210190899548365 ) ) ;
#17690=ORIENTED_EDGE ( 'NONE', *, *, #23193, .F. ) ;
#17699=SURFACE_SIDE_STYLE ('',( #8260 ) ) ;
#17722=AXIS2_PLACEMENT_3D ( 'NONE', #2627, #14015, #29203 ) ;
#17753=CARTESIAN_POINT ( 'NONE',  ( -3.221703195397895403, -1.419518900327898736, 227.6563758784881202 ) ) ;
#17790=PLANE ( 'NONE',  #8518 ) ;
#17855=SURFACE_STYLE_USAGE ( .BOTH. , #17699 ) ;
#17926=CARTESIAN_POINT ( 'NONE',  ( -1.022169856860690729, -3.500000000000000444, 227.7302799852759279 ) ) ;
#18011=( LENGTH_UNIT ( ) NAMED_UNIT ( * ) SI_UNIT ( .MILLI., .METRE. ) );
#18034=CARTESIAN_POINT ( 'NONE',  ( -3.185244259044060389, 1.482995108822391161, 230.8358029176239938 ) ) ;
#18049=EDGE_LOOP ( 'NONE', ( #1621, #10456, #29640, #15788 ) ) ;
#18085=CARTESIAN_POINT ( 'NONE',  ( 2.909761405891116315, 1.959661555859188997, 230.8336353467307447 ) ) ;
#18097=PRODUCT ( 'Nut', 'Nut', '', ( #18383 ) ) ;
#18171=AXIS2_PLACEMENT_3D ( 'NONE', #6509, #9172, #11393 ) ;
#18181=COLOUR_RGB ( '', 0.40784314, 0.44705882, 0.49803922) ;
#18215=ORIENTED_EDGE ( 'NONE', *, *, #11958, .F. ) ;
#18233=CARTESIAN_POINT ( 'NONE',  ( -3.504469657370753222, 0.9297831746172884326, 227.7188583759496794 ) ) ;
#18245=CARTESIAN_POINT ( 'NONE',  ( -2.020725942269999909, -3.500000000000000000, 227.9588918784999976 ) ) ;
#18367=CARTESIAN_POINT ( 'NONE',  ( -3.341854967535827114, 1.211737404705432564, 230.8123217011524844 ) ) ;
#18383=PRODUCT_CONTEXT ( 'NONE', #21852, 'mechanical' ) ;
#18420=CARTESIAN_POINT ( 'NONE',  ( -2.020725942159999899, 3.500000000000000000, 229.2412452703699728 ) ) ;
#18430=DIRECTION ( 'NONE',  ( 2.197671641579999817E-16, 1.000000000000000000, 0.000000000000000000 ) ) ;
#18432=B_SPLINE_CURVE_WITH_KNOTS ( 'NONE', 3,
 ( #14343, #26747, #23942, #7697, #19671, #11965, #5184, #9919, #9758, #14797, #28955 ),
 .UNSPECIFIED., .F., .F.,
 ( 4, 1, 1, 1, 2, 2, 4 ),
 ( 0.000000000000000000, 0.2499999999999971134, 0.3749999999999970579, 0.4374999999999971689, 0.4687499999999974465, 0.4999999999999977796, 1.000000000000000000 ),
 .UNSPECIFIED. ) ;
#18457=VERTEX_POINT ( 'NONE', #5575 ) ;
#18490=VECTOR ( 'NONE', #30548, 1000.000000000000000 ) ;
#18506=CARTESIAN_POINT ( 'NONE',  ( 8.881784197000000993E-16, -2.220446049249999755E-16, 227.6412452699999847 ) ) ;
#18559=CARTESIAN_POINT ( 'NONE',  ( -2.631336845234771626, 2.442053353369756152, 227.6979960600623087 ) ) ;
#18566=VERTEX_POINT ( 'NONE', #10686 ) ;
#18673=DIRECTION ( 'NONE',  ( -0.8660254037843290176, -0.5000000000001900702, -0.000000000000000000 ) ) ;
#18675=EDGE_CURVE ( 'NONE', #22953, #18690, #4750, .T. ) ;
#18678=CARTESIAN_POINT ( 'NONE',  ( 3.342478061398093114, -1.210236869212865551, 230.8050258245734199 ) ) ;
#18690=VERTEX_POINT ( 'NONE', #2353 ) ;
#18750=STYLED_ITEM ( 'NONE', ( #1200 ), #14437 ) ;
#18847=ORIENTED_EDGE ( 'NONE', *, *, #23193, .T. ) ;
#18905=CARTESIAN_POINT ( 'NONE',  ( -1.380865576431546504, 3.499743769987727404, 227.7972036410087640 ) ) ;
#18958=VECTOR ( 'NONE', #15705, 1000.000000000000227 ) ;
#18969=CARTESIAN_POINT ( 'NONE',  ( -380005.9281980000087, -207598.1847299999790, 250226.6334002700169 ) ) ;
#18995=FACE_OUTER_BOUND ( 'NONE', #18049, .T. ) ;
#19021=CARTESIAN_POINT ( 'NONE',  ( -1.022169856810371869, 3.500000000000000000, 230.7522105547308797 ) ) ;
#19178=CARTESIAN_POINT ( 'NONE',  ( 2.020725942159999899, 3.500000000000000000, 230.5235986622430175 ) ) ;
#19230=EDGE_LOOP ( 'NONE', ( #9790, #9630 ) ) ;
#19337=CARTESIAN_POINT ( 'NONE',  ( -0.9795220552175427642, 3.499999999999998668, 230.7589734104489594 ) ) ;
#19346=DIRECTION ( 'NONE',  ( 0.000000000000000000, -1.000000000000000000, 0.000000000000000000 ) ) ;
#19370=DIRECTION ( 'NONE',  ( 0.8775825618903722036, 0.4794255386042040601, 0.000000000000000000 ) ) ;
#19386=CARTESIAN_POINT ( 'NONE',  ( -0.3140692933582686641, -3.500175508915968070, 230.8361203540576128 ) ) ;
#19395=ORIENTED_EDGE ( 'NONE', *, *, #29536, .F. ) ;
#19443=CARTESIAN_POINT ( 'NONE',  ( 3.388885134111758735, 1.130278766698372905, 230.7950857227842505 ) ) ;
#19445=FACE_OUTER_BOUND ( 'NONE', #15777, .T. ) ;
#19457=CARTESIAN_POINT ( 'NONE',  ( 1.947945353336631769, 0.5234957687185587405, 227.6412452701542009 ) ) ;
#19460=AXIS2_PLACEMENT_3D ( 'NONE', #27633, #25610, #16148 ) ;
#19527=ORIENTED_EDGE ( 'NONE', *, *, #167, .F. ) ;
#19542=CARTESIAN_POINT ( 'NONE',  ( 0.8681810495234366654, -3.499839992693361435, 230.7751077600164251 ) ) ;
#19615=B_SPLINE_CURVE_WITH_KNOTS ( 'NONE', 3,
 ( #17317, #27380, #12746, #24872, #20449, #7863, #25333, #17466, #15564, #3775, #15264 ),
 .UNSPECIFIED., .F., .F.,
 ( 4, 1, 1, 1, 2, 2, 4 ),
 ( 0.000000000000000000, 0.2499999999999816258, 0.3749999999999713562, 0.4374999999999661937, 0.4687499999999662492, 0.4999999999999663602, 1.000000000000000000 ),
 .UNSPECIFIED. ) ;
#19671=CARTESIAN_POINT ( 'NONE',  ( 2.656656946665528540, 2.398535190088667335, 227.6918569120566360 ) ) ;
#19692=CARTESIAN_POINT ( 'NONE',  ( -0.9592076359448037381, -3.499847752372934995, 230.7617868067715960 ) ) ;
#19737=B_SPLINE_CURVE_WITH_KNOTS ( 'NONE', 3,
 ( #22525, #3617, #18085, #6136, #29746, #8174, #13211, #15732, #25346, #3786, #6763, #1743, #15898, #9270 ),
 .UNSPECIFIED., .F., .F.,
 ( 4, 2, 2, 1, 1, 2, 2, 4 ),
 ( 0.000000000000000000, 0.2500000000000099365, 0.3750000000000136002, 0.4375000000000135447, 0.4687500000000111022, 0.4843750000000072164, 0.5000000000000033307, 1.000000000000000000 ),
 .UNSPECIFIED. ) ;
#19884=DIRECTION ( 'NONE',  ( 0.000000000000000000, 0.000000000000000000, 1.000000000000000000 ) ) ;
#19886=ADVANCED_FACE ( 'NONE', ( #27967 ), #13333, .T. ) ;
#19913=CARTESIAN_POINT ( 'NONE',  ( 3.455669901342143024, 1.014542102255497902, 227.7047085156410162 ) ) ;
#19960=ORIENTED_EDGE ( 'NONE', *, *, #6352, .T. ) ;
#20014=EDGE_CURVE ( 'NONE', #29946, #2944, #3165, .T. ) ;
#20042=VERTEX_POINT ( 'NONE', #14898 ) ;
#20072=FACE_OUTER_BOUND ( 'NONE', #27539, .T. ) ;
#20139=CARTESIAN_POINT ( 'NONE',  ( 0.2650424577970988960, 2.000000000000000000, 230.8412452700000301 ) ) ;
#20283=CARTESIAN_POINT ( 'NONE',  ( 1.009922359840511374, -1.745934706676925297, 230.8412452700000301 ) ) ;
#20333=CARTESIAN_POINT ( 'NONE',  ( -3.072394438959999974, -1.678456730820000020, 230.8356432492296619 ) ) ;
#20435=EDGE_CURVE ( 'NONE', #24964, #27054, #518, .T. ) ;
#20449=CARTESIAN_POINT ( 'NONE',  ( -2.656656946654432971, -2.398535190107887960, 227.6918569120630593 ) ) ;
#20451=CARTESIAN_POINT ( 'NONE',  ( -3.721299799755369619, 0.5540072166027351086, 227.7972036410060639 ) ) ;
#20505=DIRECTION ( 'NONE',  ( 0.7600087925169251024, 0.4151946956549595336, 0.4999999999969509945 ) ) ;
#20536=ORIENTED_EDGE ( 'NONE', *, *, #11306, .T. ) ;
#20556=ADVANCED_FACE ( 'NONE', ( #4896 ), #14642, .T. ) ;
#20559=CARTESIAN_POINT ( 'NONE',  ( -3.072394438959999974, -1.678456730820000020, 230.8356432492296619 ) ) ;
#20566=CARTESIAN_POINT ( 'NONE',  ( -3.805699214915442052, 0.4083356014457980576, 230.6508329224847103 ) ) ;
#20598=CARTESIAN_POINT ( 'NONE',  ( 0.5207266838923305663, 1.948929461725765089, 230.8412452700000586 ) ) ;
#20729=CARTESIAN_POINT ( 'NONE',  ( -2.953785065807760457, 1.883894191386363381, 230.8358359828810364 ) ) ;
#20765=CARTESIAN_POINT ( 'NONE',  ( -3.340912886194220111, 1.213242220896334045, 227.6700366507570834 ) ) ;
#20776=CARTESIAN_POINT ( 'NONE',  ( 0.8585117870642997584, -3.500000000000000444, 227.7058346192808642 ) ) ;
#20797=PLANE ( 'NONE',  #4959 ) ;
#20805=CARTESIAN_POINT ( 'NONE',  ( -0.9470189794544437989, 3.499851337386774119, 227.7188583759513847 ) ) ;
#20885=EDGE_CURVE ( 'NONE', #7731, #27018, #19615, .T. ) ;
#20894=CARTESIAN_POINT ( 'NONE',  ( -2.700260886555499340, 2.323010950798258811, 230.8013441257832028 ) ) ;
#20928=CARTESIAN_POINT ( 'NONE',  ( -2.567750454434825080, 2.552195388715847724, 227.7157682482517771 ) ) ;
#20961=CARTESIAN_POINT ( 'NONE',  ( 0.8681810495354941315, 3.499839992690838120, 227.7073827799873982 ) ) ;
#21036=CARTESIAN_POINT ( 'NONE',  ( -3.257018533420682704, -1.358678418916599018, 230.8224594091674930 ) ) ;
#21037=UNCERTAINTY_MEASURE_WITH_UNIT (LENGTH_MEASURE( 1.000000000000000082E-05 ), #11774, 'distance_accuracy_value', 'NONE');
#21046=CARTESIAN_POINT ( 'NONE',  ( -2.687036963334896278, -2.345727656357492918, 230.7977248921665137 ) ) ;
#21070=CARTESIAN_POINT ( 'NONE',  ( 8.881784197000000993E-16, -2.220446049249999755E-16, 230.8412452700000017 ) ) ;
#21112=CARTESIAN_POINT ( 'NONE',  ( 3.224831307069992992, -1.414428330319838389, 227.6554536018044814 ) ) ;
#21205=CARTESIAN_POINT ( 'NONE',  ( 4.041451884329999800, 2.220446049249999755E-16, 230.5235986622430175 ) ) ;
#21288=EDGE_LOOP ( 'NONE', ( #27549, #6213, #26126, #4717, #29526, #24043, #14522 ) ) ;
#21360=CARTESIAN_POINT ( 'NONE',  ( 0.5234957687185571862, -1.947945353336631991, 227.6412452703391409 ) ) ;
#21394=DIRECTION ( 'NONE',  ( -0.8775825618903722036, -0.4794255386042040601, 0.000000000000000000 ) ) ;
#21555=AXIS2_PLACEMENT_3D ( 'NONE', #6253, #15856, #13485 ) ;
#21769=ORIENTED_EDGE ( 'NONE', *, *, #20885, .T. ) ;
#21806=B_SPLINE_CURVE_WITH_KNOTS ( 'NONE', 3,
 ( #9232, #25779, #28440, #4211, #6872, #30174, #25629, #9083, #23111, #28279, #27971, #11608, #4527, #4368, #16474, #30338, #18678, #23260, #23583, #16014, #2017, #3902, #4059, #8604, #26088, #21205 ),
 .UNSPECIFIED., .F., .F.,
 ( 4, 2, 2, 1, 1, 2, 2, 2, 2, 2, 1, 1, 2, 2, 4 ),
 ( 0.000000000000000000, 0.1249999999999832911, 0.1874999999999727440, 0.2187499999999673594, 0.2343749999999648337, 0.2421874999999636124, 0.2499999999999623634, 0.4999999999999558131, 0.6249999999999522604, 0.6874999999999497069, 0.7187499999999472644, 0.7343749999999473754, 0.7421874999999487077, 0.7499999999999501510, 1.000000000000000000 ),
 .UNSPECIFIED. ) ;
#21852=APPLICATION_CONTEXT ( 'automotive_design' ) ;
#21910=CARTESIAN_POINT ( 'NONE',  ( 0.7404173758759277080, -3.499814327641340927, 230.7917081009901210 ) ) ;
#21970=CARTESIAN_POINT ( 'NONE',  ( 3.333579493031019858, 1.225759174641957827, 227.6757455870668423 ) ) ;
#22222=STYLED_ITEM ( 'NONE', ( #4688 ), #540 ) ;
#22305=AXIS2_PLACEMENT_3D ( 'NONE', #4951, #29019, #2446 ) ;
#22367=EDGE_CURVE ( 'NONE', #20042, #11709, #21806, .T. ) ;
#22432=CARTESIAN_POINT ( 'NONE',  ( 3.072394438959999974, 1.678456730820000020, 227.6468472915199754 ) ) ;
#22452=ORIENTED_EDGE ( 'NONE', *, *, #9840, .F. ) ;
#22504=CARTESIAN_POINT ( 'NONE',  ( -3.455669901315109094, -1.014542102293449322, 227.7047085156324044 ) ) ;
#22525=CARTESIAN_POINT ( 'NONE',  ( 3.072394438959999974, 1.678456730820000020, 230.8356432492296619 ) ) ;
#22615=CARTESIAN_POINT ( 'NONE',  ( 2.020725942269999909, 3.500000000000000000, 229.2412452703699728 ) ) ;
#22627=FACE_OUTER_BOUND ( 'NONE', #27080, .T. ) ;
#22653=CARTESIAN_POINT ( 'NONE',  ( -3.147559148823861896, -1.548267634411989002, 227.6488953029183619 ) ) ;
#22729=CARTESIAN_POINT ( 'NONE',  ( 3.858789587625139905, 0.3163803785107239808, 230.6290587881442775 ) ) ;
#22773=MECHANICAL_DESIGN_GEOMETRIC_PRESENTATION_REPRESENTATION('',(#18750),#13213);
#22806=CARTESIAN_POINT ( 'NONE',  ( 1.009653006785187435, 1.746192186286544379, 230.8412452699999449 ) ) ;
#22819=DIRECTION ( 'NONE',  ( 0.000000000000000000, 0.000000000000000000, -1.000000000000000000 ) ) ;
#22827=CARTESIAN_POINT ( 'NONE',  ( 0.8979745064769899532, -3.500000000000000444, 227.7113415996607557 ) ) ;
#22889=CARTESIAN_POINT ( 'NONE',  ( 2.020725942159999899, -3.500000000000000000, 230.8412452700000017 ) ) ;
#22937=CARTESIAN_POINT ( 'NONE',  ( -2.215775945506506250, -3.162163484183925899, 230.6362108339131680 ) ) ;
#22953=VERTEX_POINT ( 'NONE', #14205 ) ;
#22967=CARTESIAN_POINT ( 'NONE',  ( -2.449212707639999657E-16, 2.000000000000000000, 230.8412452696274499 ) ) ;
#22978=CARTESIAN_POINT ( 'NONE',  ( -2.385386868421338402, 2.867855126291142476, 227.7701677845706740 ) ) ;
#22987=CARTESIAN_POINT ( 'NONE',  ( 1.636264169889315223, -3.499999999999998668, 227.8479073241728088 ) ) ;
#23005=CARTESIAN_POINT ( 'NONE',  ( 4.041451884329999800, 2.701186720849999812E-16, 227.9588918784999976 ) ) ;
#23064=VECTOR ( 'NONE', #2960, 1000.000000000000227 ) ;
#23100=CARTESIAN_POINT ( 'NONE',  ( -3.650178114498183746, 0.6777060490173741902, 230.7147300523249100 ) ) ;
#23111=CARTESIAN_POINT ( 'NONE',  ( 2.540292811207268020, -2.599765019149025136, 230.7583807310656994 ) ) ;
#23147=CARTESIAN_POINT ( 'NONE',  ( 0.9163752123955551943, -3.500000000000000000, 227.7139869426476082 ) ) ;
#23165=CARTESIAN_POINT ( 'NONE',  ( 3.849220998203362054, -0.3329536615551556000, 227.8479073241742583 ) ) ;
#23173=CARTESIAN_POINT ( 'NONE',  ( -2.020725942109999895, 3.500000000090000007, 227.9588918784999976 ) ) ;
#23193=EDGE_CURVE ( 'NONE', #27018, #24964, #15006, .T. ) ;
#23250=CARTESIAN_POINT ( 'NONE',  ( -2.909761405888054320, -1.959661555870369831, 230.8336353467288973 ) ) ;
#23260=CARTESIAN_POINT ( 'NONE',  ( 3.401136804196998931, -1.108686906912193182, 230.7917081009935032 ) ) ;
#23275=CARTESIAN_POINT ( 'NONE',  ( 380005.9281980000087, 207598.1847299999790, 250226.6334002700169 ) ) ;
#23290=CARTESIAN_POINT ( 'NONE',  ( -2.596859818084732208, 2.501786840328394046, 227.7073827799883361 ) ) ;
#23320=DIRECTION ( 'NONE',  ( 1.000000000000000000, -2.197671641579999817E-16, 0.000000000000000000 ) ) ;
#23331=CARTESIAN_POINT ( 'NONE',  ( 0.6231431573705923377, 3.499789347373832626, 227.6774647154332456 ) ) ;
#23350=EDGE_LOOP ( 'NONE', ( #19395, #4317 ) ) ;
#23363=B_SPLINE_CURVE_WITH_KNOTS ( 'NONE', 3,
 ( #23173, #6634, #15924, #18905, #6794, #25534, #23490, #16081, #11203, #8832, #20805, #16391, #11364, #4124, #28503, #13720, #23331, #31024, #1774, #20961, #30567, #8994, #6948, #25997, #16232, #25848 ),
 .UNSPECIFIED., .F., .F.,
 ( 4, 2, 2, 1, 1, 2, 2, 2, 2, 2, 1, 1, 2, 2, 4 ),
 ( 0.000000000000000000, 0.1249999999999871769, 0.1874999999999786282, 0.2187499999999742983, 0.2343749999999737987, 0.2421874999999750755, 0.2499999999999762967, 0.4999999999999507061, 0.6249999999999379385, 0.6874999999999308331, 0.7187499999999272804, 0.7343749999999240607, 0.7421874999999240607, 0.7499999999999240607, 1.000000000000000000 ),
 .UNSPECIFIED. ) ;
#23367=FACE_OUTER_BOUND ( 'NONE', #23513, .T. ) ;
#23406=EDGE_CURVE ( 'NONE', #8650, #22953, #3701, .T. ) ;
#23408=CARTESIAN_POINT ( 'NONE',  ( -3.388885134110333208, -1.130278766700842263, 230.7950857227854158 ) ) ;
#23456=CARTESIAN_POINT ( 'NONE',  ( -2.572138351271164414, 2.544598447946130992, 227.7144805344102849 ) ) ;
#23460=EDGE_CURVE ( 'NONE', #28246, #2338, #11994, .T. ) ;
#23481=CARTESIAN_POINT ( 'NONE',  ( 3.108392760683923228, -1.616105808619877626, 227.6466545571246343 ) ) ;
#23486=DIRECTION ( 'NONE',  ( 0.000000000000000000, 0.000000000000000000, -1.000000000000000000 ) ) ;
#23490=CARTESIAN_POINT ( 'NONE',  ( -1.091910126179790330, 3.499798787991532212, 227.7419800002291197 ) ) ;
#23513=EDGE_LOOP ( 'NONE', ( #5719, #11148, #18847, #2791 ) ) ;
#23583=CARTESIAN_POINT ( 'NONE',  ( 3.430548664023152838, -1.057777877209630901, 230.7844944799449820 ) ) ;
#23758=CARTESIAN_POINT ( 'NONE',  ( 0.000000000000000000, 0.000000000000000000, 230.8412452699534470 ) ) ;
#23821=AXIS2_PLACEMENT_3D ( 'NONE', #26726, #155, #4710 ) ;
#23885=CARTESIAN_POINT ( 'NONE',  ( 1.599333684796361066, 1.229093439949829003, 227.6412452701079019 ) ) ;
#23906=( NAMED_UNIT ( * ) PLANE_ANGLE_UNIT ( ) SI_UNIT ( $, .RADIAN. ) );
#23942=CARTESIAN_POINT ( 'NONE',  ( 2.871635305848139641, 2.026181749456782200, 227.6510696331277472 ) ) ;
#23962=CARTESIAN_POINT ( 'NONE',  ( -1.158394559326821005, -3.499774879700301433, 230.7286668686161306 ) ) ;
#23992=DIRECTION ( 'NONE',  ( 0.000000000000000000, -1.000000000000000000, 0.000000000000000000 ) ) ;
#24043=ORIENTED_EDGE ( 'NONE', *, *, #23460, .T. ) ;
#24173=B_SPLINE_CURVE_WITH_KNOTS ( 'NONE', 3,
 ( #13046, #22653, #17753, #15712, #15410, #8158, #22504, #3767, #8314, #1258, #8470, #25009, #5962 ),
 .UNSPECIFIED., .F., .F.,
 ( 4, 2, 2, 1, 2, 2, 4 ),
 ( 0.000000000000000000, 0.2499999999999729661, 0.3749999999999577005, 0.4374999999999472644, 0.4687499999999453215, 0.4999999999999433786, 1.000000000000000000 ),
 .UNSPECIFIED. ) ;
#24209=CARTESIAN_POINT ( 'NONE',  ( -1.549220603335524693, 3.500000000000000000, 230.6508329224841987 ) ) ;
#24219=LINE ( 'NONE', #28774, #2716 ) ;
#24252=CARTESIAN_POINT ( 'NONE',  ( 0.6231431573718050343, -3.499789347373825077, 230.8050258245700093 ) ) ;
#24301=FACE_BOUND ( 'NONE', #19230, .T. ) ;
#24343=DIRECTION ( 'NONE',  ( 0.000000000000000000, 0.000000000000000000, 1.000000000000000000 ) ) ;
#24350=AXIS2_PLACEMENT_3D ( 'NONE', #29661, #1341, #27149 ) ;
#24507=FILL_AREA_STYLE_COLOUR ( '', #18181 ) ;
#24571=CARTESIAN_POINT ( 'NONE',  ( 0.3123980048451518443, -3.499890163169941726, 230.8301842479583286 ) ) ;
#24601=FACE_OUTER_BOUND ( 'NONE', #30842, .T. ) ;
#24629=DIRECTION ( 'NONE',  ( 0.000000000000000000, 0.000000000000000000, -1.000000000000000000 ) ) ;
#24701=EDGE_CURVE ( 'NONE', #2338, #20042, #303, .T. ) ;
#24803=( NAMED_UNIT ( * ) SI_UNIT ( $, .STERADIAN. ) SOLID_ANGLE_UNIT ( ) );
#24816=LINE ( 'NONE', #22615, #29056 ) ;
#24872=CARTESIAN_POINT ( 'NONE',  ( -2.728640529166729944, -2.273855967885826779, 227.6754430268740634 ) ) ;
#24957=( NAMED_UNIT ( * ) PLANE_ANGLE_UNIT ( ) SI_UNIT ( $, .RADIAN. ) );
#24964=VERTEX_POINT ( 'NONE', #8640 ) ;
#25009=CARTESIAN_POINT ( 'NONE',  ( -3.862245930668567251, -0.3103938167503151324, 227.8554272724453824 ) ) ;
#25044=CARTESIAN_POINT ( 'NONE',  ( -4.041451884379999804, 9.156941871420000667E-11, 229.2412452703699728 ) ) ;
#25061=AXIS2_PLACEMENT_3D ( 'NONE', #108, #24629, #14726 ) ;
#25119=ORIENTED_EDGE ( 'NONE', *, *, #10974, .F. ) ;
#25186=CARTESIAN_POINT ( 'NONE',  ( -0.9568679087659598403, -3.500000000000000000, 227.7200428341212159 ) ) ;
#25293=CARTESIAN_POINT ( 'NONE',  ( -2.656431219428132096, -2.398832595398723289, 230.7906780663903703 ) ) ;
#25306=CARTESIAN_POINT ( 'NONE',  ( -8.424250880209998925E-16, -2.000000000000000000, 230.8412452700000017 ) ) ;
#25307=ORIENTED_EDGE ( 'NONE', *, *, #20885, .F. ) ;
#25333=CARTESIAN_POINT ( 'NONE',  ( -2.605043309123956430, -2.487932632674070721, 227.7052921205641098 ) ) ;
#25346=CARTESIAN_POINT ( 'NONE',  ( 2.605017075358218470, 2.487964477257813112, 230.7771899713955293 ) ) ;
#25368=CARTESIAN_POINT ( 'NONE',  ( 2.876933567438932027, -2.017004891198901362, 227.6466876223813927 ) ) ;
#25449=CARTESIAN_POINT ( 'NONE',  ( -3.511914029060239528, -0.9171864698486590362, 230.7613442533420596 ) ) ;
#25453=ORIENTED_EDGE ( 'NONE', *, *, #29536, .T. ) ;
#25487=CARTESIAN_POINT ( 'NONE',  ( 0.5204573308370086249, -1.949186941335384837, 230.8412452700000301 ) ) ;
#25534=CARTESIAN_POINT ( 'NONE',  ( -1.158394559368730592, 3.499774879702899799, 227.7538236713963897 ) ) ;
#25607=CARTESIAN_POINT ( 'NONE',  ( -3.455337460955915319, -1.015179960323179920, 230.7778176299147788 ) ) ;
#25610=DIRECTION ( 'NONE',  ( 0.000000000000000000, 0.000000000000000000, 1.000000000000000000 ) ) ;
#25629=CARTESIAN_POINT ( 'NONE',  ( 2.484959595460734860, -2.695521301889526544, 230.7405105397797342 ) ) ;
#25659=CARTESIAN_POINT ( 'NONE',  ( -3.188275555100174241, 1.478095767874147759, 227.6463701859477453 ) ) ;
#25738=ORIENTED_EDGE ( 'NONE', *, *, #16254, .T. ) ;
#25756=DIRECTION ( 'NONE',  ( 0.000000000000000000, 0.000000000000000000, 1.000000000000000000 ) ) ;
#25770=CARTESIAN_POINT ( 'NONE',  ( -2.990544846594861639, -1.820224383388544531, 230.8378734041664586 ) ) ;
#25779=CARTESIAN_POINT ( 'NONE',  ( 2.114469059363687009, -3.337632158144848482, 230.5777212759258248 ) ) ;
#25796=EDGE_CURVE ( 'NONE', #18566, #18690, #19737, .T. ) ;
#25817=VECTOR ( 'NONE', #22819, 1000.000000000000000 ) ;
#25838=CARTESIAN_POINT ( 'NONE',  ( 2.541327885618866134, -2.598290983419757172, 227.7235171295553471 ) ) ;
#25845=LINE ( 'NONE', #4282, #30928 ) ;
#25848=CARTESIAN_POINT ( 'NONE',  ( 2.020725942159999899, 3.500000000000000000, 227.9588918784999976 ) ) ;
#25988=EDGE_CURVE ( 'NONE', #26221, #2944, #24219, .T. ) ;
#25997=CARTESIAN_POINT ( 'NONE',  ( 1.290941959520814475, 3.499733189051936755, 227.7701677845689119 ) ) ;
#26025=VECTOR ( 'NONE', #12390, 1000.000000000000000 ) ;
#26088=CARTESIAN_POINT ( 'NONE',  ( 3.853987913886425698, -0.3246971213886250540, 230.6318310357701193 ) ) ;
#26126=ORIENTED_EDGE ( 'NONE', *, *, #14101, .T. ) ;
#26221=VERTEX_POINT ( 'NONE', #25306 ) ;
#26263=CARTESIAN_POINT ( 'NONE',  ( -1.828693153457167320, 3.499999999999999112, 230.5790337530978888 ) ) ;
#26313=CARTESIAN_POINT ( 'NONE',  ( -1.091910126141098170, -3.499798787989274462, 230.7405105397821785 ) ) ;
#26509=FACE_OUTER_BOUND ( 'NONE', #7429, .T. ) ;
#26530=ADVANCED_FACE ( 'NONE', ( #18995 ), #17097, .T. ) ;
#26648=DIRECTION ( 'NONE',  ( 0.000000000000000000, 0.000000000000000000, 1.000000000000000000 ) ) ;
#26726=CARTESIAN_POINT ( 'NONE',  ( 0.000000000000000000, 0.000000000000000000, 230.8412452699534470 ) ) ;
#26747=CARTESIAN_POINT ( 'NONE',  ( 2.992535305844774118, 1.816776806827645085, 227.6446713698604185 ) ) ;
#26844=ADVANCED_FACE ( 'NONE', ( #24301, #26509 ), #4640, .F. ) ;
#26931=CARTESIAN_POINT ( 'NONE',  ( -1.291648043245374966, -3.499742528933395658, 230.7036791710427508 ) ) ;
#27008=FILL_AREA_STYLE ('',( #27462 ) ) ;
#27018=VERTEX_POINT ( 'NONE', #27586 ) ;
#27054=VERTEX_POINT ( 'NONE', #6501 ) ;
#27080=EDGE_LOOP ( 'NONE', ( #17690, #25307, #12585, #12758, #25119, #25738, #12862 ) ) ;
#27096=CARTESIAN_POINT ( 'NONE',  ( -2.020725942269999909, -3.500000000000000000, 230.5235986622430175 ) ) ;
#27149=DIRECTION ( 'NONE',  ( -1.224646799149999836E-16, 1.000000000000000000, 0.000000000000000000 ) ) ;
#27242=ORIENTED_EDGE ( 'NONE', *, *, #2351, .F. ) ;
#27296=CARTESIAN_POINT ( 'NONE',  ( 3.691781163184647330, 0.6055607618373975987, 227.7772386881597697 ) ) ;
#27380=CARTESIAN_POINT ( 'NONE',  ( -2.992535305846383054, -1.816776806824856427, 227.6446713698603617 ) ) ;
#27447=CYLINDRICAL_SURFACE ( 'NONE', #24350, 2.000000000000000000 ) ;
#27462=FILL_AREA_STYLE_COLOUR ( '', #1169 ) ;
#27539=EDGE_LOOP ( 'NONE', ( #977, #15246, #9012, #7759 ) ) ;
#27549=ORIENTED_EDGE ( 'NONE', *, *, #22367, .T. ) ;
#27586=CARTESIAN_POINT ( 'NONE',  ( -2.020725942269999909, -3.500000000000000000, 227.9588918784999976 ) ) ;
#27633=CARTESIAN_POINT ( 'NONE',  ( -8.881784197000000993E-16, 2.220446049249999755E-16, 227.6412452699999847 ) ) ;
#27661=VERTEX_POINT ( 'NONE', #30644 ) ;
#27708=CARTESIAN_POINT ( 'NONE',  ( 2.020725942159999899, -3.500000000000000000, 227.9588918784999976 ) ) ;
#27720=CIRCLE ( 'NONE', #18171, 2.000000000000000000 ) ;
#27737=LINE ( 'NONE', #9593, #3925 ) ;
#27802=CARTESIAN_POINT ( 'NONE',  ( -2.605017075328921017, -2.487964477322084811, 230.7771899713821426 ) ) ;
#27832=CARTESIAN_POINT ( 'NONE',  ( 1.746002136800675508, 1.009759976939816672, 230.8412452700000017 ) ) ;
#27920=DIRECTION ( 'NONE',  ( 0.000000000000000000, 0.000000000000000000, -1.000000000000000000 ) ) ;
#27955=CARTESIAN_POINT ( 'NONE',  ( -3.145769537975008578, -1.551367331319410514, 230.8336439985933453 ) ) ;
#27967=FACE_OUTER_BOUND ( 'NONE', #334, .T. ) ;
#27971=CARTESIAN_POINT ( 'NONE',  ( 2.557450677934476779, -2.570068162742275231, 230.7636321640558208 ) ) ;
#28112=EDGE_CURVE ( 'NONE', #8534, #27661, #13208, .T. ) ;
#28156=ADVANCED_FACE ( 'NONE', ( #24601 ), #3034, .T. ) ;
#28246=VERTEX_POINT ( 'NONE', #20333 ) ;
#28270=CARTESIAN_POINT ( 'NONE',  ( -2.582101660013529365, 2.527668734551885787, 230.7711489403428970 ) ) ;
#28279=CARTESIAN_POINT ( 'NONE',  ( 2.551353244962082822, -2.580622056418603094, 230.7617868067710276 ) ) ;
#28291=DIRECTION ( 'NONE',  ( 0.000000000000000000, 0.000000000000000000, 1.000000000000000000 ) ) ;
#28295=LINE ( 'NONE', #23275, #18958 ) ;
#28310=CARTESIAN_POINT ( 'NONE',  ( -2.660719428328687020, 2.391127420732980013, 227.6907824390136170 ) ) ;
#28321=EDGE_CURVE ( 'NONE', #15258, #29368, #23363, .T. ) ;
#28337=CARTESIAN_POINT ( 'NONE',  ( 3.480076166481417488, -0.9723312654487008544, 227.7113415996591925 ) ) ;
#28435=CARTESIAN_POINT ( 'NONE',  ( 1.229093439949830335, 1.599333684796359956, 227.6412452700770928 ) ) ;
#28440=CARTESIAN_POINT ( 'NONE',  ( 2.205637557623687073, -3.179374645688476164, 230.6249086619264688 ) ) ;
#28503=CARTESIAN_POINT ( 'NONE',  ( 0.3123980048345580962, 3.499890163171272661, 227.6523062920452958 ) ) ;
#28561=AXIS2_PLACEMENT_3D ( 'NONE', #1174, #27920, #15336 ) ;
#28593=CARTESIAN_POINT ( 'NONE',  ( 1.599333684796359067, -1.229093439949832334, 227.6412452702620897 ) ) ;
#28622=CARTESIAN_POINT ( 'NONE',  ( -1.086409578978756896, 3.499999999999999556, 230.7417114753006047 ) ) ;
#28725=CARTESIAN_POINT ( 'NONE',  ( 3.483928249571823343, 0.9656592618119906879, 230.7696496080370423 ) ) ;
#28753=SURFACE_SIDE_STYLE ('',( #454 ) ) ;
#28774=CARTESIAN_POINT ( 'NONE',  ( 4.898425415290000099E-16, -2.000000000000000000, 229.2412452703699728 ) ) ;
#28898=CARTESIAN_POINT ( 'NONE',  ( 1.087346358790000053E-15, 2.000000000000000000, 227.6412452699999847 ) ) ;
#28928=CARTESIAN_POINT ( 'NONE',  ( 0.9163752123637586289, 3.499999999999999556, 230.7685035973587446 ) ) ;
#28955=CARTESIAN_POINT ( 'NONE',  ( 2.020725942159999899, 3.500000000000000000, 227.9588918784999976 ) ) ;
#28976=CARTESIAN_POINT ( 'NONE',  ( -0.9813161448490499428, -3.499840617129381659, 230.7583807310667225 ) ) ;
#29002=CIRCLE ( 'NONE', #19460, 3.491271820589999741 ) ;
#29019=DIRECTION ( 'NONE',  ( 0.000000000000000000, 0.000000000000000000, -1.000000000000000000 ) ) ;
#29034=CARTESIAN_POINT ( 'NONE',  ( 3.503013490861627499, 0.9326026542233571970, 230.7640337244206421 ) ) ;
#29050=CARTESIAN_POINT ( 'NONE',  ( 1.007237960741796279, -1.747572776708517406, 227.6412452703083886 ) ) ;
#29056=VECTOR ( 'NONE', #8585, 1000.000000000000000 ) ;
#29080=CARTESIAN_POINT ( 'NONE',  ( 0.7993620172799370538, 3.499999999999998668, 230.7846409045036751 ) ) ;
#29088=DIRECTION ( 'NONE',  ( 0.000000000000000000, 0.000000000000000000, -1.000000000000000000 ) ) ;
#29203=DIRECTION ( 'NONE',  ( 1.000000000000000000, 0.000000000000000000, 0.000000000000000000 ) ) ;
#29253=EDGE_LOOP ( 'NONE', ( #4335, #674 ) ) ;
#29276=CARTESIAN_POINT ( 'NONE',  ( -0.9470189794284002982, -3.499851337386873595, 230.7636321640559913 ) ) ;
#29319=EDGE_CURVE ( 'NONE', #11709, #27054, #8482, .T. ) ;
#29368=VERTEX_POINT ( 'NONE', #30207 ) ;
#29468=ADVANCED_FACE ( 'NONE', ( #14931 ), #1689, .T. ) ;
#29526=ORIENTED_EDGE ( 'NONE', *, *, #11545, .F. ) ;
#29536=EDGE_CURVE ( 'NONE', #2944, #29946, #5693, .T. ) ;
#29601=ORIENTED_EDGE ( 'NONE', *, *, #7104, .F. ) ;
#29640=ORIENTED_EDGE ( 'NONE', *, *, #20435, .T. ) ;
#29653=FACE_BOUND ( 'NONE', #23350, .T. ) ;
#29659=CARTESIAN_POINT ( 'NONE',  ( 3.503090509817559539, 0.9324612816629570533, 227.7184664424436846 ) ) ;
#29661=CARTESIAN_POINT ( 'NONE',  ( 0.000000000000000000, 0.000000000000000000, 229.2412452700000074 ) ) ;
#29746=CARTESIAN_POINT ( 'NONE',  ( 2.748065355789120812, 2.239845275076990827, 230.8106057538952598 ) ) ;
#29884=CARTESIAN_POINT ( 'NONE',  ( 1.999932741570970673, 0.2648802556752510307, 230.8412452700000017 ) ) ;
#29946=VERTEX_POINT ( 'NONE', #31111 ) ;
#30000=CARTESIAN_POINT ( 'NONE',  ( -2.393497562785666055, 2.854340613466038512, 230.7151724862272602 ) ) ;
#30037=CARTESIAN_POINT ( 'NONE',  ( 1.601210460384887568, 1.226419552957089820, 230.8412452700000301 ) ) ;
#30148=ORIENTED_EDGE ( 'NONE', *, *, #18675, .F. ) ;
#30163=CARTESIAN_POINT ( 'NONE',  ( -4.041451884379999804, 9.156941871420000667E-11, 230.5235986622430175 ) ) ;
#30174=CARTESIAN_POINT ( 'NONE',  ( 2.451696673680768157, -2.753086555842796379, 230.7286668686129190 ) ) ;
#30196=CARTESIAN_POINT ( 'NONE',  ( 1.948929461725908752, -0.5207266838928901187, 230.8412452700000301 ) ) ;
#30207=CARTESIAN_POINT ( 'NONE',  ( 2.020725942159999899, 3.500000000000000000, 227.9588918784999976 ) ) ;
#30338=CARTESIAN_POINT ( 'NONE',  ( 3.303595366871416417, -1.277580108374672951, 230.8124249489373199 ) ) ;
#30356=CARTESIAN_POINT ( 'NONE',  ( 4.041451884329999800, 2.220446049249999755E-16, 230.5235986622430175 ) ) ;
#30373=CARTESIAN_POINT ( 'NONE',  ( -2.952483221433048310, 1.886467326085379925, 227.6463841914517729 ) ) ;
#30383=CARTESIAN_POINT ( 'NONE',  ( -0.3083106916347965742, -3.499999999999999556, 227.6466876223823874 ) ) ;
#30406=CARTESIAN_POINT ( 'NONE',  ( -2.020725942159999899, 3.500000000000000000, 230.8412452700000017 ) ) ;
#30548=DIRECTION ( 'NONE',  ( 0.000000000000000000, 0.000000000000000000, -1.000000000000000000 ) ) ;
#30567=CARTESIAN_POINT ( 'NONE',  ( 0.8978302376703681809, 3.499838689518511625, 227.7116136946774247 ) ) ;
#30581=ORIENTED_EDGE ( 'NONE', *, *, #11958, .T. ) ;
#30595=B_SPLINE_CURVE_WITH_KNOTS ( 'NONE', 3,
 ( #22967, #20139, #20598, #22806, #10854, #30037, #27832, #1414, #29884, #6435, #30196, #6283, #10689, #15884, #20283, #25487, #3923, #13517 ),
 .UNSPECIFIED., .F., .F.,
 ( 4, 2, 2, 2, 2, 2, 2, 2, 4 ),
 ( 0.000000000000000000, 0.1250000000000000000, 0.2500000000000000000, 0.3750000000000000000, 0.5000000000000000000, 0.6250000000000000000, 0.7500000000000000000, 0.8750000000000000000, 1.000000000000000000 ),
 .UNSPECIFIED. ) ;
#30644=CARTESIAN_POINT ( 'NONE',  ( 3.063879268240000009, 1.673804873600000187, 230.8412452700000017 ) ) ;
#30646=CARTESIAN_POINT ( 'NONE',  ( -2.590102362109455658, -2.513801395391271676, 230.7730491447685210 ) ) ;
#30651=CARTESIAN_POINT ( 'NONE',  ( -2.020725942159999899, -3.500000000000000000, 230.8412452700000017 ) ) ;
#30696=ORIENTED_EDGE ( 'NONE', *, *, #11306, .F. ) ;
#30708=CARTESIAN_POINT ( 'NONE',  ( 3.430769921896569929, -1.057732186200032176, 227.6978496355009725 ) ) ;
#30748=PRODUCT_DEFINITION_CONTEXT ( 'detailed design', #1352, 'design' ) ;
#30842=EDGE_LOOP ( 'NONE', ( #5606, #16019, #14201, #27242 ) ) ;
#30928=VECTOR ( 'NONE', #23486, 1000.000000000000000 ) ;
#30946=ORIENTED_EDGE ( 'NONE', *, *, #12673, .F. ) ;
#30955=CARTESIAN_POINT ( 'NONE',  ( 0.2617993877991457441, -2.000000000000001332, 227.6412452703546592 ) ) ;
#31001=VERTEX_POINT ( 'NONE', #6139 ) ;
#31024=CARTESIAN_POINT ( 'NONE',  ( 0.7404173758804706296, 3.499814327640350609, 227.6907824390132760 ) ) ;
#31031=CARTESIAN_POINT ( 'NONE',  ( 2.020725942159999899, -3.500000000000000000, 230.5235986622430175 ) ) ;
#31094=CARTESIAN_POINT ( 'NONE',  ( 3.145769537974499208, 1.551367331320289145, 230.8336439985931179 ) ) ;
#31111=CARTESIAN_POINT ( 'NONE',  ( 1.087346358790000053E-15, 2.000000000000000000, 227.6412452699999847 ) ) ;
ENDSEC;
END-ISO-10303-21;
